ISO-10303-21;
HEADER;
FILE_DESCRIPTION (('STEP AP214'),
    '1' );
FILE_NAME ('Chuck Key Tool.step',
    '2026-10-09T08:48:44',
    ( '' ),
    ( '' ),
    'SwSTEP 2.0',
    'SolidWorks 2026',
    '' );
FILE_SCHEMA (( 'AUTOMOTIVE_DESIGN' ));
ENDSEC;

DATA;
#31=CARTESIAN_POINT ( 'NONE',  ( -0.2597599741900292747, 0.1405915162213216552, 5.593567858643829993 ) ) ;
#93=CARTESIAN_POINT ( 'NONE',  ( -0.2945219335573386332, -0.02405856270293451477, 5.877884953661866696 ) ) ;
#174=EDGE_CURVE ( 'NONE', #2979, #51820, #28890, .T. ) ;
#292=ORIENTED_EDGE ( 'NONE', *, *, #19718, .F. ) ;
#313=ORIENTED_EDGE ( 'NONE', *, *, #50172, .F. ) ;
#366=CIRCLE ( 'NONE', #79699, 0.2755905511811031494 ) ;
#500=( BOUNDED_CURVE ( )  B_SPLINE_CURVE ( 3, ( #56843, #36672, #56026, #75410 ),
 .UNSPECIFIED., .F., .F. ) 
 B_SPLINE_CURVE_WITH_KNOTS ( ( 4, 4 ),
 ( 0.000000000000000000, 0.6251940424154354137 ),
 .UNSPECIFIED. ) 
 CURVE ( )  GEOMETRIC_REPRESENTATION_ITEM ( )  RATIONAL_B_SPLINE_CURVE ( ( 1.000000000000000000, 0.9676920770090842172, 0.9676920770090842172, 1.000000000000000000 ) ) 
 REPRESENTATION_ITEM ( '' )  );
#587=CARTESIAN_POINT ( 'NONE',  ( 0.2950900605411925781, -0.01202116872835604609, 5.525111687089955481 ) ) ;
#704=CARTESIAN_POINT ( 'NONE',  ( 0.1323808228461570424, -0.2647380121165202049, 0.1574803149606299746 ) ) ;
#727=CARTESIAN_POINT ( 'NONE',  ( -0.1938976377952756625, -0.1938976377952756625, 0.07874015748031495954 ) ) ;
#835=CARTESIAN_POINT ( 'NONE',  ( 1.948818897637795367, 0.000000000000000000, 5.701968306260621233 ) ) ;
#895=VERTEX_POINT ( 'NONE', #75675 ) ;
#926=CARTESIAN_POINT ( 'NONE',  ( 1.968503937007874072, 0.000000000000000000, 5.701968306260621233 ) ) ;
#1014=CARTESIAN_POINT ( 'NONE',  ( 0.2952755905511810774, 3.179810529374183920E-17, 5.879133660591329580 ) ) ;
#1125=EDGE_LOOP ( 'NONE', ( #30642, #47090, #57720, #8607 ) ) ;
#1225=DIRECTION ( 'NONE',  ( -0.000000000000000000, -1.000000000000000000, -0.000000000000000000 ) ) ;
#1256=DIRECTION ( 'NONE',  ( 1.000000000000000000, 0.000000000000000000, 0.000000000000000000 ) ) ;
#1295=CARTESIAN_POINT ( 'NONE',  ( -0.2635443281053753695, 0.1334515064332122414, 5.819037890265706281 ) ) ;
#1334=DIRECTION ( 'NONE',  ( 0.5773502691896310601, -0.5773502691896310601, -0.5773502691896149619 ) ) ;
#1410=CIRCLE ( 'NONE', #37669, 0.1574803149606300579 ) ;
#1451=EDGE_LOOP ( 'NONE', ( #12170, #38807, #56909, #39319 ) ) ;
#1622=CARTESIAN_POINT ( 'NONE',  ( 0.2952755905511810774, 3.616083068348483797E-17, 6.062992125984251857 ) ) ;
#1703=CARTESIAN_POINT ( 'NONE',  ( -0.2407525580057141290, 0.1709688663325618363, 5.655154502652836257 ) ) ;
#1753=CYLINDRICAL_SURFACE ( 'NONE', #53035, 0.1771653543307088186 ) ;
#1869=LINE ( 'NONE', #27531, #11538 ) ;
#2127=DIRECTION ( 'NONE',  ( -1.000000000000000000, 0.000000000000000000, 0.000000000000000000 ) ) ;
#2222=( BOUNDED_CURVE ( )  B_SPLINE_CURVE ( 3, ( #62120, #23815, #36447, #22584 ),
 .UNSPECIFIED., .F., .F. ) 
 B_SPLINE_CURVE_WITH_KNOTS ( ( 4, 4 ),
 ( 0.000000000000000000, 0.6251940424154347475 ),
 .UNSPECIFIED. ) 
 CURVE ( )  GEOMETRIC_REPRESENTATION_ITEM ( )  RATIONAL_B_SPLINE_CURVE ( ( 1.000000000000000000, 0.9676920770090842172, 0.9676920770090842172, 1.000000000000000000 ) ) 
 REPRESENTATION_ITEM ( '' )  );
#2223=DIRECTION ( 'NONE',  ( 0.000000000000000000, -0.7071067811865376918, 0.7071067811865573427 ) ) ;
#2323=AXIS2_PLACEMENT_3D ( 'NONE', #5498, #17736, #57233 ) ;
#2342=ADVANCED_FACE ( 'NONE', ( #25780 ), #58181, .T. ) ;
#2406=DIRECTION ( 'NONE',  ( 0.000000000000000000, 0.000000000000000000, 1.000000000000000000 ) ) ;
#2483=VERTEX_POINT ( 'NONE', #78829 ) ;
#2495=CARTESIAN_POINT ( 'NONE',  ( 0.2952755905511810774, 3.597759587968672259E-17, 5.524802951929911998 ) ) ;
#2516=EDGE_CURVE ( 'NONE', #22229, #4461, #79229, .T. ) ;
#2564=CARTESIAN_POINT ( 'NONE',  ( 0.2710655044954047299, -0.1174279065223611668, 5.568826803765086986 ) ) ;
#2627=PLANE ( 'NONE',  #12150 ) ;
#2826=CARTESIAN_POINT ( 'NONE',  ( 0.1990279662527742466, 0.1990279662527742466, 0.1112963449492364726 ) ) ;
#2894=ORIENTED_EDGE ( 'NONE', *, *, #75879, .T. ) ;
#2906=CARTESIAN_POINT ( 'NONE',  ( 0.2814587350932031828, 0.08983405572796258898, 5.548838678696989213 ) ) ;
#2975=CARTESIAN_POINT ( 'NONE',  ( 0.2917579853797115930, -0.04689358074580353419, 5.530719428720964892 ) ) ;
#2979=VERTEX_POINT ( 'NONE', #15685 ) ;
#3164=ORIENTED_EDGE ( 'NONE', *, *, #174, .F. ) ;
#3225=DIRECTION ( 'NONE',  ( -1.000000000000000000, -0.000000000000000000, -0.000000000000000000 ) ) ;
#3369=DIRECTION ( 'NONE',  ( -6.226572250490765667E-17, 0.7071067811865368036, 0.7071067811865582309 ) ) ;
#3455=B_SPLINE_CURVE_WITH_KNOTS ( 'NONE', 3,
 ( #23915, #23498, #74870, #82006, #18029, #55062, #80770, #62634, #17213, #10879 ),
 .UNSPECIFIED., .F., .F.,
 ( 4, 2, 2, 2, 4 ),
 ( 0.000000000000000000, 0.001551611299846701337, 0.002327416949770050921, 0.002715319774731725280, 0.003103222599693400072 ),
 .UNSPECIFIED. ) ;
#3525=TOROIDAL_SURFACE ( 'NONE', #45125, 0.1574803149606295860, 0.01968503937007873988 ) ;
#3594=CARTESIAN_POINT ( 'NONE',  ( -0.1752652180395700143, -0.2378425880835044193, 0.1496354662858539464 ) ) ;
#3622=ORIENTED_EDGE ( 'NONE', *, *, #38964, .T. ) ;
#3730=CARTESIAN_POINT ( 'NONE',  ( 0.2952755905511811885, 0.01200600163628318291, 5.879133660591329580 ) ) ;
#3894=CARTESIAN_POINT ( 'NONE',  ( 0.000000000000000000, 0.000000000000000000, 0.1574803149606299191 ) ) ;
#4050=EDGE_LOOP ( 'NONE', ( #80768, #13992, #26789, #62532, #23547, #82750, #11274, #56192, #18075, #78345, #74104, #51839, #74536, #66950 ) ) ;
#4163=AXIS2_PLACEMENT_3D ( 'NONE', #20077, #40268, #21329 ) ;
#4204=CARTESIAN_POINT ( 'NONE',  ( -0.2952755905511810774, -3.179810529374183920E-17, 5.879133660591329580 ) ) ;
#4217=FACE_OUTER_BOUND ( 'NONE', #63842, .T. ) ;
#4301=DIRECTION ( 'NONE',  ( 1.000000000000000000, 8.805702923740138355E-17, 0.000000000000000000 ) ) ;
#4461=VERTEX_POINT ( 'NONE', #42182 ) ;
#4494=ORIENTED_EDGE ( 'NONE', *, *, #64155, .T. ) ;
#4744=CARTESIAN_POINT ( 'NONE',  ( -0.2524666497344155158, -0.1533018367440332486, 5.791491733107224427 ) ) ;
#4835=ADVANCED_FACE ( 'NONE', ( #64019 ), #6360, .F. ) ;
#4873=LENGTH_MEASURE_WITH_UNIT ( LENGTH_MEASURE( 0.02539999999999999897 ), #76000 );
#4895=CIRCLE ( 'NONE', #53246, 0.2952755905511810774 ) ;
#4909=ORIENTED_EDGE ( 'NONE', *, *, #50636, .F. ) ;
#4928=CARTESIAN_POINT ( 'NONE',  ( 0.2378425880835043915, -0.1752652180395700143, 0.1496354662858539464 ) ) ;
#5004=DIRECTION ( 'NONE',  ( 0.000000000000000000, -1.000000000000000000, 0.000000000000000000 ) ) ;
#5025=VERTEX_POINT ( 'NONE', #56043 ) ;
#5124=SURFACE_STYLE_FILL_AREA ( #25706 ) ;
#5151=ORIENTED_EDGE ( 'NONE', *, *, #174, .T. ) ;
#5165=CARTESIAN_POINT ( 'NONE',  ( -0.2490413359174502850, -0.1587297840844698882, 5.622433025490734870 ) ) ;
#5373=LINE ( 'NONE', #6190, #36365 ) ;
#5498=CARTESIAN_POINT ( 'NONE',  ( 1.968503937007874072, 0.000000000000000000, 5.701968306260621233 ) ) ;
#5572=CARTESIAN_POINT ( 'NONE',  ( -0.2917302971764580977, -0.04706822171083040879, 5.873170128030149151 ) ) ;
#5816=CARTESIAN_POINT ( 'NONE',  ( 0.2142011206082509167, 0.2032823926810629067, 0.1316721176867485521 ) ) ;
#5856=AXIS2_PLACEMENT_3D ( 'NONE', #19280, #44931, #6652 ) ;
#5869=CARTESIAN_POINT ( 'NONE',  ( 0.1938976377952755792, -0.1938976377952756069, 0.1574803149606299191 ) ) ;
#5942=( NAMED_UNIT ( * ) SI_UNIT ( $, .STERADIAN. ) SOLID_ANGLE_UNIT ( ) );
#6190=CARTESIAN_POINT ( 'NONE',  ( -0.2952755905511810774, 0.000000000000000000, 6.062992125984251857 ) ) ;
#6324=ADVANCED_FACE ( 'NONE', ( #41763 ), #73360, .F. ) ;
#6336=CARTESIAN_POINT ( 'NONE',  ( -0.2814773692359251456, 0.08976595949324576995, 5.548806511850565393 ) ) ;
#6359=( CONVERSION_BASED_UNIT ( 'INCH', #56455 ) LENGTH_UNIT ( ) NAMED_UNIT ( #62602 ) );
#6360=CYLINDRICAL_SURFACE ( 'NONE', #32509, 0.07874015748031495954 ) ;
#6373=PLANE ( 'NONE',  #70860 ) ;
#6652=DIRECTION ( 'NONE',  ( 0.000000000000000000, 0.000000000000000000, 1.000000000000000000 ) ) ;
#6682=MANIFOLD_SOLID_BREP ( 'Fillet2', #39322 ) ;
#6711=DIRECTION ( 'NONE',  ( 0.000000000000000000, 0.000000000000000000, -1.000000000000000000 ) ) ;
#6766=APPLICATION_CONTEXT ( 'automotive_design' ) ;
#6787=CARTESIAN_POINT ( 'NONE',  ( 0.000000000000000000, 0.000000000000000000, 0.1574803149606299191 ) ) ;
#6789=CARTESIAN_POINT ( 'NONE',  ( -0.2229926280064457034, -0.1936066689571366572, 0.1399704324547693945 ) ) ;
#6827=CARTESIAN_POINT ( 'NONE',  ( -0.2726377952755906220, -0.1133856558944467546, 0.1574803149606299191 ) ) ;
#6888=CARTESIAN_POINT ( 'NONE',  ( 0.2635551335312363852, -0.1334335510540912706, 5.584872361112684480 ) ) ;
#6936=DIRECTION ( 'NONE',  ( 0.000000000000000000, 1.000000000000000000, -0.000000000000000000 ) ) ;
#7132=VECTOR ( 'NONE', #48788, 39.37007874015748143 ) ;
#7173=CARTESIAN_POINT ( 'NONE',  ( -1.968503937007874072, 0.000000000000000000, 5.701968306260621233 ) ) ;
#7356=CARTESIAN_POINT ( 'NONE',  ( 0.1938976377952755792, -0.1938976377952756069, -0.3740157480314971750 ) ) ;
#7398=ADVANCED_FACE ( 'NONE', ( #7629 ), #13560, .T. ) ;
#7425=ORIENTED_EDGE ( 'NONE', *, *, #16767, .F. ) ;
#7603=CARTESIAN_POINT ( 'NONE',  ( -0.2445414048442310917, 0.1655124888405462291, 5.638514421976805302 ) ) ;
#7629=FACE_OUTER_BOUND ( 'NONE', #1451, .T. ) ;
#7646=FACE_OUTER_BOUND ( 'NONE', #41699, .T. ) ;
#7721=CARTESIAN_POINT ( 'NONE',  ( 0.1938976377952755792, -0.2726377952755905665, 0.1574803149606299191 ) ) ;
#7785=DIRECTION ( 'NONE',  ( 0.000000000000000000, 0.000000000000000000, 1.000000000000000000 ) ) ;
#7924=DIRECTION ( 'NONE',  ( 0.000000000000000000, 0.000000000000000000, 1.000000000000000000 ) ) ;
#8021=CARTESIAN_POINT ( 'NONE',  ( -0.2431769186048377551, 0.1675026378872651045, 5.643961825897842566 ) ) ;
#8115=DIRECTION ( 'NONE',  ( -1.000000000000000000, 0.000000000000000000, 0.000000000000000000 ) ) ;
#8244=B_SPLINE_CURVE_WITH_KNOTS ( 'NONE', 3,
 ( #18218, #75470, #70798, #18623, #30829, #81790, #57730, #43853, #50994, #62831, #82600, #82196, #5165, #37146, #50181, #56494, #32069, #11492, #36729, #45094, #56085, #62405, #24917, #24513, #44266, #77111, #4744, #19444, #51409, #75876, #69957, #24101, #49770, #69556, #17810, #11904, #5572, #93, #43443, #76692 ),
 .UNSPECIFIED., .F., .F.,
 ( 4, 2, 2, 2, 2, 2, 2, 2, 2, 2, 2, 2, 2, 2, 2, 2, 2, 2, 2, 4 ),
 ( 0.01443715752414749011, 0.01533768712752721711, 0.01623821673090694584, 0.01713874633428667110, 0.01803927593766639637, 0.01893980554104612163, 0.01984033514442585036, 0.02029059994611567483, 0.02074086474780550277, 0.02119112954949533070, 0.02164139435118515864, 0.02254192395456481104, 0.02344245355794446345, 0.02434298316132411932, 0.02524351276470376826, 0.02614404236808342413, 0.02659430716977325207, 0.02704457197146308001, 0.02794510157484273241, 0.02884563117822238482 ),
 .UNSPECIFIED. ) ;
#8268=CARTESIAN_POINT ( 'NONE',  ( 0.2061694042878472188, -0.2114133405073580219, 0.1284558427095352229 ) ) ;
#8598=DIRECTION ( 'NONE',  ( -1.000000000000000000, -8.805702923740138355E-17, 0.000000000000000000 ) ) ;
#8607=ORIENTED_EDGE ( 'NONE', *, *, #38964, .F. ) ;
#8723=CARTESIAN_POINT ( 'NONE',  ( 0.000000000000000000, 0.000000000000000000, 6.043307086614173151 ) ) ;
#8767=EDGE_CURVE ( 'NONE', #65017, #55450, #26188, .T. ) ;
#8802=CARTESIAN_POINT ( 'NONE',  ( 0.2373513483963055337, 0.1756490242921440736, 5.678081160219037749 ) ) ;
#8871=CARTESIAN_POINT ( 'NONE',  ( 0.2845351084527213970, -0.07967650482972132853, 5.860631297047876664 ) ) ;
#8909=DIRECTION ( 'NONE',  ( -0.000000000000000000, -0.000000000000000000, -1.000000000000000000 ) ) ;
#9017=FACE_OUTER_BOUND ( 'NONE', #36036, .T. ) ;
#9022=CARTESIAN_POINT ( 'NONE',  ( 0.000000000000000000, 0.000000000000000000, 0.1574803149606299191 ) ) ;
#9116=ORIENTED_EDGE ( 'NONE', *, *, #12655, .F. ) ;
#9136=CARTESIAN_POINT ( 'NONE',  ( 0.000000000000000000, 0.000000000000000000, 0.000000000000000000 ) ) ;
#9221=CARTESIAN_POINT ( 'NONE',  ( 0.2747288752779719623, 0.1086799599621180723, 5.842342907282080056 ) ) ;
#9312=ORIENTED_EDGE ( 'NONE', *, *, #38110, .T. ) ;
#9342=DIRECTION ( 'NONE',  ( -1.000000000000000000, -8.805702923740138355E-17, 0.000000000000000000 ) ) ;
#9351=DIRECTION ( 'NONE',  ( 0.000000000000000000, 0.000000000000000000, 1.000000000000000000 ) ) ;
#9530=CARTESIAN_POINT ( 'NONE',  ( 0.000000000000000000, 0.000000000000000000, 6.043307086614173151 ) ) ;
#9537=ADVANCED_FACE ( 'NONE', ( #47625 ), #41329, .F. ) ;
#9570=EDGE_CURVE ( 'NONE', #79188, #18348, #35424, .T. ) ;
#9591=VECTOR ( 'NONE', #72487, 39.37007874015748143 ) ;
#9703=CARTESIAN_POINT ( 'NONE',  ( 0.2407525580057140735, -0.1709688663325618085, 5.655154502652835369 ) ) ;
#9876=DIRECTION ( 'NONE',  ( 0.000000000000000000, -1.000000000000000000, 0.000000000000000000 ) ) ;
#10040=CARTESIAN_POINT ( 'NONE',  ( -0.2755905511811031494, 0.000000000000000000, 6.062992125984251857 ) ) ;
#10048=CARTESIAN_POINT ( 'NONE',  ( 0.2896968578984297493, 0.05818598865049057212, 5.869712490931006776 ) ) ;
#10166=AXIS2_PLACEMENT_3D ( 'NONE', #59869, #2223, #27888 ) ;
#10185=CARTESIAN_POINT ( 'NONE',  ( 0.000000000000000000, 0.000000000000000000, 0.1574803149606299191 ) ) ;
#10205=EDGE_CURVE ( 'NONE', #77294, #74332, #4895, .T. ) ;
#10216=CARTESIAN_POINT ( 'NONE',  ( -1.948818897637795367, 0.000000000000000000, 5.701968306260621233 ) ) ;
#10261=VECTOR ( 'NONE', #1225, 39.37007874015748143 ) ;
#10282=CARTESIAN_POINT ( 'NONE',  ( -0.1938976377952756625, 0.1938976377952755792, -0.3740157480314971750 ) ) ;
#10326=AXIS2_PLACEMENT_3D ( 'NONE', #30091, #74314, #42716 ) ;
#10390=AXIS2_PLACEMENT_3D ( 'NONE', #26498, #71956, #71534 ) ;
#10513=EDGE_CURVE ( 'NONE', #47374, #79188, #54319, .T. ) ;
#10528=ORIENTED_EDGE ( 'NONE', *, *, #10513, .T. ) ;
#10553=CARTESIAN_POINT ( 'NONE',  ( 0.000000000000000000, 0.000000000000000000, 6.062992125984251857 ) ) ;
#10617=CARTESIAN_POINT ( 'NONE',  ( 1.968503937007874072, 0.000000000000000000, 5.879133660591329580 ) ) ;
#10678=CARTESIAN_POINT ( 'NONE',  ( 1.534064387305127072E-17, -0.1742125984251973736, -0.3937007874015748254 ) ) ;
#10742=CARTESIAN_POINT ( 'NONE',  ( -0.2035438835850315042, -0.2140388612101737920, 0.1320934087364891429 ) ) ;
#10858=EDGE_LOOP ( 'NONE', ( #46512, #46650, #26275, #46230 ) ) ;
#10879=CARTESIAN_POINT ( 'NONE',  ( -0.2087913723976025926, 0.2087913723976025371, 0.1248231986745539646 ) ) ;
#10882=B_SPLINE_CURVE_WITH_KNOTS ( 'NONE', 3,
 ( #71193, #78354, #63621, #45072, #70775, #6789, #26146, #32885, #31628, #52230 ),
 .UNSPECIFIED., .F., .F.,
 ( 4, 2, 2, 2, 4 ),
 ( 0.000000000000000000, 0.001551611299846700686, 0.002327416949770050921, 0.002715319774731726581, 0.003103222599693402674 ),
 .UNSPECIFIED. ) ;
#11019=EDGE_CURVE ( 'NONE', #55450, #32253, #69687, .T. ) ;
#11204=DIRECTION ( 'NONE',  ( -1.000000000000000000, 0.000000000000000000, 0.000000000000000000 ) ) ;
#11252=CARTESIAN_POINT ( 'NONE',  ( 0.2198823481317033202, -0.1972978822260922083, 0.1376690760605703834 ) ) ;
#11274=ORIENTED_EDGE ( 'NONE', *, *, #61486, .T. ) ;
#11286=DIRECTION ( 'NONE',  ( -0.000000000000000000, -0.000000000000000000, -1.000000000000000000 ) ) ;
#11325=CARTESIAN_POINT ( 'NONE',  ( -0.1133856558944468518, -0.2726377952755905665, 0.1574803149606299191 ) ) ;
#11345=ADVANCED_FACE ( 'NONE', ( #13275 ), #38927, .F. ) ;
#11347=AXIS2_PLACEMENT_3D ( 'NONE', #35222, #48664, #66385 ) ;
#11370=DIRECTION ( 'NONE',  ( -1.000000000000000000, 0.000000000000000000, 0.000000000000000000 ) ) ;
#11480=VECTOR ( 'NONE', #71260, 39.37007874015748143 ) ;
#11492=CARTESIAN_POINT ( 'NONE',  ( -0.2380158072512372769, -0.1747520019874606034, 5.672240063627636886 ) ) ;
#11527=DIRECTION ( 'NONE',  ( -1.000000000000000000, -0.000000000000000000, -0.000000000000000000 ) ) ;
#11538=VECTOR ( 'NONE', #53187, 39.37007874015748143 ) ;
#11553=VERTEX_POINT ( 'NONE', #46482 ) ;
#11605=CARTESIAN_POINT ( 'NONE',  ( -0.1938976377952756625, -0.1938976377952756625, -0.3740157480314971750 ) ) ;
#11904=CARTESIAN_POINT ( 'NONE',  ( -0.2896968578984297493, -0.05818598865049063457, 5.869712490931005888 ) ) ;
#11909=ORIENTED_EDGE ( 'NONE', *, *, #47802, .F. ) ;
#12024=CARTESIAN_POINT ( 'NONE',  ( 0.1938976377952755792, 0.1938976377952755792, -0.3740157480314971750 ) ) ;
#12084=ORIENTED_EDGE ( 'NONE', *, *, #34230, .F. ) ;
#12148=CARTESIAN_POINT ( 'NONE',  ( 0.2379288306351265703, 0.1751536117528152414, 0.1496817530000226493 ) ) ;
#12150=AXIS2_PLACEMENT_3D ( 'NONE', #10185, #9351, #53945 ) ;
#12170=ORIENTED_EDGE ( 'NONE', *, *, #66747, .F. ) ;
#12208=B_SPLINE_CURVE_WITH_KNOTS ( 'NONE', 3,
 ( #51869, #65371, #14447, #38836, #40098, #20322, #20745, #59037, #64515, #58184 ),
 .UNSPECIFIED., .F., .F.,
 ( 4, 2, 2, 2, 4 ),
 ( 0.000000000000000000, 0.0007778963758021331535, 0.001555792751604266307, 0.002333689127406399569, 0.003111585503208532614 ),
 .UNSPECIFIED. ) ;
#12270=( LENGTH_UNIT ( ) NAMED_UNIT ( * ) SI_UNIT ( $, .METRE. ) );
#12540=EDGE_CURVE ( 'NONE', #21842, #11553, #17432, .T. ) ;
#12655=EDGE_CURVE ( 'NONE', #19415, #66357, #34525, .T. ) ;
#12665=CARTESIAN_POINT ( 'NONE',  ( 0.1938976377952755792, -0.1938976377952756069, -0.3740157480314971750 ) ) ;
#12685=SURFACE_STYLE_USAGE ( .BOTH. , #24061 ) ;
#12694=ORIENTED_EDGE ( 'NONE', *, *, #47802, .T. ) ;
#12730=ORIENTED_EDGE ( 'NONE', *, *, #12540, .F. ) ;
#12777=DIRECTION ( 'NONE',  ( 1.000000000000000000, 0.000000000000000000, 0.000000000000000000 ) ) ;
#12896=LINE ( 'NONE', #38555, #80452 ) ;
#13224=CARTESIAN_POINT ( 'NONE',  ( 0.2490243534527243618, -0.1587552710309117210, 5.781441956045568986 ) ) ;
#13275=FACE_OUTER_BOUND ( 'NONE', #43228, .T. ) ;
#13560=CONICAL_SURFACE ( 'NONE', #18947, 0.2755905511811031494, 0.7853981633974284060 ) ;
#13707=EDGE_CURVE ( 'NONE', #55729, #33736, #19728, .T. ) ;
#13801=APPLICATION_CONTEXT ( 'automotive_design' ) ;
#13835=TOROIDAL_SURFACE ( 'NONE', #39346, 0.1574803149606295860, 0.01968503937007873988 ) ;
#13921=CARTESIAN_POINT ( 'NONE',  ( -0.2490243534527243618, 0.1587552710309117210, 5.781441956045568986 ) ) ;
#13961=DIRECTION ( 'NONE',  ( 0.000000000000000000, 0.000000000000000000, 1.000000000000000000 ) ) ;
#13992=ORIENTED_EDGE ( 'NONE', *, *, #10205, .T. ) ;
#14245=CARTESIAN_POINT ( 'NONE',  ( 0.2952755905511810774, 3.616083068348483797E-17, 6.043307086614173151 ) ) ;
#14293=CIRCLE ( 'NONE', #62644, 0.01968503937007875723 ) ;
#14345=CARTESIAN_POINT ( 'NONE',  ( -0.2405786259268995197, 0.1712252042737591462, 5.748956133594166573 ) ) ;
#14393=DIRECTION ( 'NONE',  ( 1.000000000000000000, 0.000000000000000000, 0.000000000000000000 ) ) ;
#14447=CARTESIAN_POINT ( 'NONE',  ( -0.2198823481317032369, 0.1972978822260920972, 0.1376690760605703279 ) ) ;
#14474=AXIS2_PLACEMENT_3D ( 'NONE', #68212, #30716, #11370 ) ;
#14532=AXIS2_PLACEMENT_3D ( 'NONE', #58094, #47138, #53031 ) ;
#14576=CARTESIAN_POINT ( 'NONE',  ( 0.2755905511811031494, 3.375010863791927619E-17, 6.062992125984251857 ) ) ;
#14758=CARTESIAN_POINT ( 'NONE',  ( -0.2371319115525430399, 0.1759675087575592878, 5.678257627497697690 ) ) ;
#14926=ORIENTED_EDGE ( 'NONE', *, *, #60899, .F. ) ;
#14954=ADVANCED_FACE ( 'NONE', ( #48457 ), #42148, .T. ) ;
#14997=ORIENTED_EDGE ( 'NONE', *, *, #43522, .T. ) ;
#15032=ORIENTED_EDGE ( 'NONE', *, *, #25885, .T. ) ;
#15191=CARTESIAN_POINT ( 'NONE',  ( 0.000000000000000000, 0.000000000000000000, 6.062992125984251857 ) ) ;
#15196=CARTESIAN_POINT ( 'NONE',  ( 0.2362173824511233644, -0.1771694743175191433, 5.690029434716978862 ) ) ;
#15207=AXIS2_PLACEMENT_3D ( 'NONE', #7173, #28195, #79566 ) ;
#15413=ORIENTED_EDGE ( 'NONE', *, *, #61486, .F. ) ;
#15533=ORIENTED_EDGE ( 'NONE', *, *, #36633, .F. ) ;
#15544=CARTESIAN_POINT ( 'NONE',  ( 0.2635274766024540694, 0.1334916279589803412, 5.819004606509203370 ) ) ;
#15597=FACE_OUTER_BOUND ( 'NONE', #33436, .T. ) ;
#15615=CARTESIAN_POINT ( 'NONE',  ( 0.2845256677560920044, -0.07972153265861246785, 5.543321648279010638 ) ) ;
#15685=CARTESIAN_POINT ( 'NONE',  ( 1.948818897637795367, 2.169649841009080787E-17, 5.524802951929911998 ) ) ;
#15712=FACE_OUTER_BOUND ( 'NONE', #64445, .T. ) ;
#15962=CARTESIAN_POINT ( 'NONE',  ( 0.2710828156362889985, 0.1173918767474883690, 5.835147349599718147 ) ) ;
#16004=DIRECTION ( 'NONE',  ( 0.000000000000000000, 0.000000000000000000, -1.000000000000000000 ) ) ;
#16030=CARTESIAN_POINT ( 'NONE',  ( 0.2952755905511810774, 3.597759587968672259E-17, 5.524802951929911998 ) ) ;
#16346=ORIENTED_EDGE ( 'NONE', *, *, #10513, .F. ) ;
#16371=CARTESIAN_POINT ( 'NONE',  ( 0.2813683484248658551, 0.08970734455876072655, 5.854851642268653400 ) ) ;
#16375=VERTEX_POINT ( 'NONE', #42865 ) ;
#16379=VERTEX_POINT ( 'NONE', #36976 ) ;
#16579=ORIENTED_EDGE ( 'NONE', *, *, #66747, .T. ) ;
#16701=CARTESIAN_POINT ( 'NONE',  ( 0.1972978822260920695, 0.2198823481317033202, 0.1376690760605704111 ) ) ;
#16767=EDGE_CURVE ( 'NONE', #17617, #21842, #63066, .T. ) ;
#17005=CARTESIAN_POINT ( 'NONE',  ( 0.000000000000000000, 0.000000000000000000, 0.1574803149606299191 ) ) ;
#17090=EDGE_CURVE ( 'NONE', #70570, #16375, #21174, .T. ) ;
#17213=CARTESIAN_POINT ( 'NONE',  ( -0.2061694042878472743, 0.2114133405073579941, 0.1284558427095351396 ) ) ;
#17268=EDGE_CURVE ( 'NONE', #2483, #65017, #46189, .T. ) ;
#17281=ORIENTED_EDGE ( 'NONE', *, *, #11019, .T. ) ;
#17375=EDGE_LOOP ( 'NONE', ( #46472, #55670, #58351, #17281 ) ) ;
#17407=CYLINDRICAL_SURFACE ( 'NONE', #50658, 0.2952755905511810774 ) ;
#17432=LINE ( 'NONE', #10282, #45243 ) ;
#17506=ORIENTED_EDGE ( 'NONE', *, *, #76145, .F. ) ;
#17571=CARTESIAN_POINT ( 'NONE',  ( 0.2140388612101737920, -0.2035438835850314487, 0.1320934087364891707 ) ) ;
#17590=( GEOMETRIC_REPRESENTATION_CONTEXT ( 3 ) GLOBAL_UNCERTAINTY_ASSIGNED_CONTEXT ( ( #60484 ) ) GLOBAL_UNIT_ASSIGNED_CONTEXT ( ( #6359, #38344, #5942 ) ) REPRESENTATION_CONTEXT ( 'NONE', 'WORKASPACE' ) );
#17602=LINE ( 'NONE', #10040, #51520 ) ;
#17617=VERTEX_POINT ( 'NONE', #25578 ) ;
#17736=DIRECTION ( 'NONE',  ( -1.000000000000000000, -0.000000000000000000, -0.000000000000000000 ) ) ;
#17778=ORIENTED_EDGE ( 'NONE', *, *, #9570, .T. ) ;
#17810=CARTESIAN_POINT ( 'NONE',  ( -0.2858256400101373829, -0.07430968296373896553, 5.862902060615214239 ) ) ;
#18029=CARTESIAN_POINT ( 'NONE',  ( -0.1829408352246092440, 0.2319625946588664833, 0.1465682319128801259 ) ) ;
#18056=CARTESIAN_POINT ( 'NONE',  ( 1.948818897637795367, 0.000000000000000000, 5.701968306260621233 ) ) ;
#18075=ORIENTED_EDGE ( 'NONE', *, *, #82328, .T. ) ;
#18218=CARTESIAN_POINT ( 'NONE',  ( -0.2952755905511810774, 1.832348042626885162E-19, 5.524802951929911998 ) ) ;
#18348=VERTEX_POINT ( 'NONE', #56947 ) ;
#18362=AXIS2_PLACEMENT_3D ( 'NONE', #68760, #45128, #69986 ) ;
#18394=CARTESIAN_POINT ( 'NONE',  ( 0.2726377952755905665, -0.1133856558944469489, 0.1574803149606299191 ) ) ;
#18496=FACE_OUTER_BOUND ( 'NONE', #47706, .T. ) ;
#18554=EDGE_CURVE ( 'NONE', #28061, #73460, #39994, .T. ) ;
#18623=CARTESIAN_POINT ( 'NONE',  ( -0.2917632292039850639, -0.04688088360317040765, 5.530710407408372831 ) ) ;
#18831=ADVANCED_FACE ( 'NONE', ( #66201 ), #26214, .F. ) ;
#18921=EDGE_CURVE ( 'NONE', #23282, #42893, #38843, .T. ) ;
#18947=AXIS2_PLACEMENT_3D ( 'NONE', #15191, #58961, #26128 ) ;
#19214=CARTESIAN_POINT ( 'NONE',  ( 0.2032823926810630177, -0.2142011206082510000, 0.1316721176867485521 ) ) ;
#19239=ORIENTED_EDGE ( 'NONE', *, *, #50213, .F. ) ;
#19272=CARTESIAN_POINT ( 'NONE',  ( 0.2647380121165202049, 0.1323808228461571257, 0.1574803149606299746 ) ) ;
#19280=CARTESIAN_POINT ( 'NONE',  ( 0.1938976377952755792, -0.1938976377952756069, 0.1574803149606299191 ) ) ;
#19294=CARTESIAN_POINT ( 'NONE',  ( -0.1938976377952756625, -0.1938976377952756625, 0.07874015748031495954 ) ) ;
#19338=VECTOR ( 'NONE', #4301, 39.37007874015748143 ) ;
#19380=CARTESIAN_POINT ( 'NONE',  ( -0.2596916824146293656, 0.1407161764240515978, 5.810203857714900444 ) ) ;
#19415=VERTEX_POINT ( 'NONE', #47233 ) ;
#19418=CARTESIAN_POINT ( 'NONE',  ( -0.1938976377952756625, 0.1938976377952755792, 0.07874015748031495954 ) ) ;
#19429=CARTESIAN_POINT ( 'NONE',  ( 0.2726377952755905665, -0.1133856558944469489, 0.1574803149606299191 ) ) ;
#19442=CIRCLE ( 'NONE', #11347, 0.1771653543307088186 ) ;
#19444=CARTESIAN_POINT ( 'NONE',  ( -0.2597269936800725709, -0.1406511682536830121, 5.810287953473523892 ) ) ;
#19494=CARTESIAN_POINT ( 'NONE',  ( -1.948818897637795367, 0.000000000000000000, 5.701968306260621233 ) ) ;
#19516=CARTESIAN_POINT ( 'NONE',  ( 0.2445414048442311472, -0.1655124888405462846, 5.638514421976807078 ) ) ;
#19560=SHAPE_REPRESENTATION_RELATIONSHIP ( 'NONE' , 'NONE' ,  #61632, #56452 ) ;
#19638=EDGE_CURVE ( 'NONE', #78367, #43096, #500, .T. ) ;
#19673=AXIS2_PLACEMENT_3D ( 'NONE', #57179, #82881, #73589 ) ;
#19702=PLANE ( 'NONE',  #20663 ) ;
#19718=EDGE_CURVE ( 'NONE', #5025, #18348, #69085, .T. ) ;
#19728=CIRCLE ( 'NONE', #65415, 0.2952755905511810774 ) ;
#19796=VECTOR ( 'NONE', #79265, 39.37007874015748143 ) ;
#19884=DIRECTION ( 'NONE',  ( 1.000000000000000000, 0.000000000000000000, 0.000000000000000000 ) ) ;
#19917=VECTOR ( 'NONE', #74179, 39.37007874015748143 ) ;
#20077=CARTESIAN_POINT ( 'NONE',  ( -1.948818897637795367, 1.928577636452520604E-17, 5.859448621221250875 ) ) ;
#20079=ADVANCED_FACE ( 'NONE', ( #65224 ), #43702, .T. ) ;
#20127=PLANE ( 'NONE',  #5856 ) ;
#20223=CARTESIAN_POINT ( 'NONE',  ( -0.2896728340831399851, 0.05829427551933642065, 5.869670624399383030 ) ) ;
#20272=ORIENTED_EDGE ( 'NONE', *, *, #75879, .F. ) ;
#20291=EDGE_CURVE ( 'NONE', #23282, #4461, #58471, .T. ) ;
#20322=CARTESIAN_POINT ( 'NONE',  ( -0.2491186766705762723, 0.1588297147721999536, 0.1541304905092664712 ) ) ;
#20357=CARTESIAN_POINT ( 'NONE',  ( 0.2371566215357294449, -0.1759343135753352327, 5.725906639596368919 ) ) ;
#20497=DIRECTION ( 'NONE',  ( 1.000000000000000000, -0.000000000000000000, -0.000000000000000000 ) ) ;
#20541=CARTESIAN_POINT ( 'NONE',  ( 1.948818897637795367, 1.928577636452520604E-17, 5.859448621221250875 ) ) ;
#20547=FACE_OUTER_BOUND ( 'NONE', #46734, .T. ) ;
#20579=ORIENTED_EDGE ( 'NONE', *, *, #64155, .F. ) ;
#20644=CARTESIAN_POINT ( 'NONE',  ( -0.2362173824511233644, 0.1771694743175191988, 5.690029434716977974 ) ) ;
#20663=AXIS2_PLACEMENT_3D ( 'NONE', #57987, #7924, #63897 ) ;
#20715=EDGE_CURVE ( 'NONE', #51820, #41668, #80338, .T. ) ;
#20745=CARTESIAN_POINT ( 'NONE',  ( -0.2544983382031791863, 0.1500752278769512393, 0.1555222293686583102 ) ) ;
#20829=EDGE_CURVE ( 'NONE', #28560, #11553, #53510, .T. ) ;
#21057=CARTESIAN_POINT ( 'NONE',  ( -0.2814827926786539480, 0.08976297916237283014, 5.855142794233184844 ) ) ;
#21076=ORIENTED_EDGE ( 'NONE', *, *, #76295, .T. ) ;
#21125=VECTOR ( 'NONE', #59576, 39.37007874015748854 ) ;
#21130=VECTOR ( 'NONE', #64729, 39.37007874015748143 ) ;
#21174=LINE ( 'NONE', #7721, #19796 ) ;
#21235=CARTESIAN_POINT ( 'NONE',  ( 1.948818897637795367, 0.000000000000000000, 5.544487991299990703 ) ) ;
#21329=DIRECTION ( 'NONE',  ( 0.000000000000000000, 1.224646799147351482E-16, 1.000000000000000000 ) ) ;
#21343=EDGE_CURVE ( 'NONE', #2483, #11553, #81486, .T. ) ;
#21375=CARTESIAN_POINT ( 'NONE',  ( 0.2755905511811031494, 3.495546966070205708E-17, 6.062992125984251857 ) ) ;
#21497=CARTESIAN_POINT ( 'NONE',  ( 0.1938976377952755792, 0.1938976377952755792, 0.07874015748031495954 ) ) ;
#21838=CARTESIAN_POINT ( 'NONE',  ( 0.2430399508222474414, 0.1677739497468299368, 5.760042173782278674 ) ) ;
#21842=VERTEX_POINT ( 'NONE', #25027 ) ;
#21911=CARTESIAN_POINT ( 'NONE',  ( 0.2597599741900292747, -0.1405915162213216552, 5.593567858643828217 ) ) ;
#21944=VECTOR ( 'NONE', #69819, 39.37007874015748143 ) ;
#22098=AXIS2_PLACEMENT_3D ( 'NONE', #9136, #2406, #28064 ) ;
#22156=CARTESIAN_POINT ( 'NONE',  ( 0.1938976377952755792, 0.1938976377952755792, -0.3740157480314971750 ) ) ;
#22226=LINE ( 'NONE', #34863, #10261 ) ;
#22229=VERTEX_POINT ( 'NONE', #26700 ) ;
#22336=EDGE_LOOP ( 'NONE', ( #2894, #52771, #69276, #57517 ) ) ;
#22460=ADVANCED_FACE ( 'NONE', ( #9017 ), #59932, .F. ) ;
#22584=CARTESIAN_POINT ( 'NONE',  ( -0.2087913723976026203, -0.2087913723976025926, 0.1248231986745540339 ) ) ;
#22722=CARTESIAN_POINT ( 'NONE',  ( -0.1938976377952756625, -0.1938976377952756625, -0.3740157480314971750 ) ) ;
#22777=EDGE_CURVE ( 'NONE', #55729, #16379, #1869, .T. ) ;
#22780=ADVANCED_FACE ( 'NONE', ( #78901 ), #46877, .F. ) ;
#22947=ADVANCED_FACE ( 'NONE', ( #74239 ), #49780, .T. ) ;
#23120=CARTESIAN_POINT ( 'NONE',  ( 0.2952755905511810774, 3.616083068348483797E-17, 6.062992125984251857 ) ) ;
#23161=DIRECTION ( 'NONE',  ( 1.000000000000000000, 0.000000000000000000, 0.000000000000000000 ) ) ;
#23260=EDGE_CURVE ( 'NONE', #32253, #2483, #55264, .T. ) ;
#23282=VERTEX_POINT ( 'NONE', #23287 ) ;
#23287=CARTESIAN_POINT ( 'NONE',  ( -0.2952755905511810774, 1.832348042626885162E-19, 5.524802951929911998 ) ) ;
#23366=TOROIDAL_SURFACE ( 'NONE', #58321, 0.1574803149606295860, 0.01968503937007873988 ) ;
#23405=CARTESIAN_POINT ( 'NONE',  ( 0.2087913723976025926, 0.2087913723976026203, 0.1248231986745541033 ) ) ;
#23498=CARTESIAN_POINT ( 'NONE',  ( -0.1323808228461572090, 0.2647380121165202049, 0.1574803149606299746 ) ) ;
#23517=DIRECTION ( 'NONE',  ( -0.000000000000000000, -0.000000000000000000, -1.000000000000000000 ) ) ;
#23547=ORIENTED_EDGE ( 'NONE', *, *, #20291, .T. ) ;
#23692=VERTEX_POINT ( 'NONE', #6827 ) ;
#23718=AXIS2_PLACEMENT_3D ( 'NONE', #7356, #64601, #6936 ) ;
#23797=ORIENTED_EDGE ( 'NONE', *, *, #81662, .T. ) ;
#23815=CARTESIAN_POINT ( 'NONE',  ( -0.1938976377952756625, -0.1938976377952756625, 0.09542247959850377881 ) ) ;
#23817=AXIS2_PLACEMENT_3D ( 'NONE', #6787, #13961, #71608 ) ;
#23904=CARTESIAN_POINT ( 'NONE',  ( 1.968503937007874072, 0.000000000000000000, 5.544487991299990703 ) ) ;
#23915=CARTESIAN_POINT ( 'NONE',  ( -0.1133856558944469489, 0.2726377952755905665, 0.1574803149606299191 ) ) ;
#24039=CARTESIAN_POINT ( 'NONE',  ( -0.2952755905511811885, 0.01202990275164721352, 5.879133660591332244 ) ) ;
#24061=SURFACE_SIDE_STYLE ('',( #5124 ) ) ;
#24087=ORIENTED_EDGE ( 'NONE', *, *, #2516, .F. ) ;
#24101=CARTESIAN_POINT ( 'NONE',  ( -0.2797625792873952855, -0.09458053269141719621, 5.851882566737991453 ) ) ;
#24130=CARTESIAN_POINT ( 'NONE',  ( 0.000000000000000000, 0.000000000000000000, 6.062992125984251857 ) ) ;
#24223=( NAMED_UNIT ( * ) SI_UNIT ( $, .STERADIAN. ) SOLID_ANGLE_UNIT ( ) );
#24513=CARTESIAN_POINT ( 'NONE',  ( -0.2405540237485361554, -0.1712599301372657035, 5.748856329247442609 ) ) ;
#24917=CARTESIAN_POINT ( 'NONE',  ( -0.2371198560983138193, -0.1759840215932895469, 5.725591907046409190 ) ) ;
#25019=ORIENTED_EDGE ( 'NONE', *, *, #56144, .T. ) ;
#25027=CARTESIAN_POINT ( 'NONE',  ( -0.1938976377952756625, 0.1938976377952755792, -0.3740157480314971750 ) ) ;
#25166=( BOUNDED_CURVE ( )  B_SPLINE_CURVE ( 3, ( #31625, #52227, #57286, #19418 ),
 .UNSPECIFIED., .F., .F. ) 
 B_SPLINE_CURVE_WITH_KNOTS ( ( 4, 4 ),
 ( 2.516398611174360145, 3.141592653589793116 ),
 .UNSPECIFIED. ) 
 CURVE ( )  GEOMETRIC_REPRESENTATION_ITEM ( )  RATIONAL_B_SPLINE_CURVE ( ( 1.000000000000000000, 0.9676920770090844393, 0.9676920770090844393, 1.000000000000000000 ) ) 
 REPRESENTATION_ITEM ( '' )  );
#25168=DIRECTION ( 'NONE',  ( 1.000000000000000000, 0.000000000000000000, 0.000000000000000000 ) ) ;
#25498=EDGE_CURVE ( 'NONE', #18348, #21842, #40284, .T. ) ;
#25504=CARTESIAN_POINT ( 'NONE',  ( 0.2087913723976025926, -0.2087913723976025926, 0.1248231986745540617 ) ) ;
#25578=CARTESIAN_POINT ( 'NONE',  ( -0.1938976377952756625, 0.1938976377952755792, 0.07874015748031495954 ) ) ;
#25586=FACE_OUTER_BOUND ( 'NONE', #53601, .T. ) ;
#25668=CARTESIAN_POINT ( 'NONE',  ( -1.948818897637795367, 2.169649841009080787E-17, 5.524802951929911998 ) ) ;
#25684=CARTESIAN_POINT ( 'NONE',  ( -0.2943720246490709735, 0.02382778696830940499, 5.526312367533047443 ) ) ;
#25706=FILL_AREA_STYLE ('',( #57690 ) ) ;
#25780=FACE_OUTER_BOUND ( 'NONE', #4050, .T. ) ;
#25885=EDGE_CURVE ( 'NONE', #47374, #19415, #35107, .T. ) ;
#25940=CARTESIAN_POINT ( 'NONE',  ( 0.1936066689571366572, -0.2229926280064456756, 0.1399704324547694778 ) ) ;
#25993=UNCERTAINTY_MEASURE_WITH_UNIT (LENGTH_MEASURE( 1.000000000000000082E-05 ), #57438, 'distance_accuracy_value', 'NONE');
#25998=ADVANCED_FACE ( 'NONE', ( #52367 ), #63764, .F. ) ;
#26128=DIRECTION ( 'NONE',  ( -1.000000000000000000, 0.000000000000000000, 0.000000000000000000 ) ) ;
#26146=CARTESIAN_POINT ( 'NONE',  ( -0.2199809220305531665, -0.1970133122064496867, 0.1374248322900812891 ) ) ;
#26155=DIRECTION ( 'NONE',  ( 0.000000000000000000, 0.000000000000000000, 1.000000000000000000 ) ) ;
#26183=DIRECTION ( 'NONE',  ( 0.000000000000000000, 0.000000000000000000, 1.000000000000000000 ) ) ;
#26188=LINE ( 'NONE', #45537, #9591 ) ;
#26214=PLANE ( 'NONE',  #10166 ) ;
#26220=DIRECTION ( 'NONE',  ( 0.000000000000000000, 0.000000000000000000, -1.000000000000000000 ) ) ;
#26243=CARTESIAN_POINT ( 'NONE',  ( 0.2746814661183891726, -0.1088119808354341550, 5.842252906343563090 ) ) ;
#26275=ORIENTED_EDGE ( 'NONE', *, *, #63069, .T. ) ;
#26355=ORIENTED_EDGE ( 'NONE', *, *, #23260, .F. ) ;
#26487=LINE ( 'NONE', #5869, #65011 ) ;
#26498=CARTESIAN_POINT ( 'NONE',  ( 0.2726377952755905665, 0.000000000000000000, 0.07874015748031495954 ) ) ;
#26530=ADVANCED_FACE ( 'NONE', ( #51530 ), #77233, .F. ) ;
#26575=DIRECTION ( 'NONE',  ( 0.000000000000000000, 0.000000000000000000, -1.000000000000000000 ) ) ;
#26667=CARTESIAN_POINT ( 'NONE',  ( 0.2814827926786539480, -0.08976297916237284402, 5.855142794233184844 ) ) ;
#26700=CARTESIAN_POINT ( 'NONE',  ( -0.2726377952755906220, 0.1133856558944467546, 0.1574803149606299191 ) ) ;
#26789=ORIENTED_EDGE ( 'NONE', *, *, #27779, .T. ) ;
#26945=CARTESIAN_POINT ( 'NONE',  ( -0.2950900605411925781, 0.01202116872835609987, 5.525111687089956369 ) ) ;
#26955=LINE ( 'NONE', #52618, #70980 ) ;
#27010=STYLED_ITEM ( 'NONE', ( #37517 ), #6682 ) ;
#27531=CARTESIAN_POINT ( 'NONE',  ( 0.2726377952755905665, 0.1938976377952755792, 0.1574803149606299191 ) ) ;
#27624=ORIENTED_EDGE ( 'NONE', *, *, #40980, .F. ) ;
#27643=CARTESIAN_POINT ( 'NONE',  ( 1.968503937007874072, 2.169649841009086334E-17, 5.524802951929911998 ) ) ;
#27685=ORIENTED_EDGE ( 'NONE', *, *, #70567, .F. ) ;
#27740=CARTESIAN_POINT ( 'NONE',  ( 0.2952755905511810774, 0.01196537350834422572, 5.524802951929911110 ) ) ;
#27779=EDGE_CURVE ( 'NONE', #74332, #52953, #5373, .T. ) ;
#27782=CARTESIAN_POINT ( 'NONE',  ( -1.948818897637795367, 0.000000000000000000, 5.701968306260621233 ) ) ;
#27888=DIRECTION ( 'NONE',  ( -1.000000000000000000, 0.000000000000000000, 0.000000000000000000 ) ) ;
#28061=VERTEX_POINT ( 'NONE', #23904 ) ;
#28064=DIRECTION ( 'NONE',  ( 1.000000000000000000, 0.000000000000000000, 0.000000000000000000 ) ) ;
#28125=COLOUR_RGB ( '', 0.66274510, 0.83137255, 0.94901961) ;
#28155=CARTESIAN_POINT ( 'NONE',  ( 0.2524556255358376688, 0.1533185143264484962, 5.612478741320920506 ) ) ;
#28195=DIRECTION ( 'NONE',  ( -1.000000000000000000, -0.000000000000000000, -0.000000000000000000 ) ) ;
#28222=CARTESIAN_POINT ( 'NONE',  ( 0.2896989933648236315, -0.05817964957694448519, 5.534220241493013503 ) ) ;
#28430=CIRCLE ( 'NONE', #75490, 0.2952755905511810774 ) ;
#28458=ORIENTED_EDGE ( 'NONE', *, *, #11019, .F. ) ;
#28487=CARTESIAN_POINT ( 'NONE',  ( 0.1938976377952756069, 0.1938976377952756069, 0.09542247959850377881 ) ) ;
#28560=VERTEX_POINT ( 'NONE', #727 ) ;
#28570=CARTESIAN_POINT ( 'NONE',  ( 0.2364516566766633465, 0.1768582946180018156, 5.689955017551601379 ) ) ;
#28641=CARTESIAN_POINT ( 'NONE',  ( 0.2635443281053753695, -0.1334515064332121859, 5.819037890265706281 ) ) ;
#28812=DIRECTION ( 'NONE',  ( 0.7071067811865376918, 0.000000000000000000, 0.7071067811865573427 ) ) ;
#28873=ORIENTED_EDGE ( 'NONE', *, *, #38110, .F. ) ;
#28890=LINE ( 'NONE', #27643, #67585 ) ;
#28979=CARTESIAN_POINT ( 'NONE',  ( 0.2596871853482274894, 0.1407230452551245514, 5.593746434152945035 ) ) ;
#29088=CARTESIAN_POINT ( 'NONE',  ( -0.1938976377952756625, -0.1938976377952756625, 0.1574803149606299191 ) ) ;
#29298=LINE ( 'NONE', #22156, #63851 ) ;
#29556=DIRECTION ( 'NONE',  ( 1.000000000000000000, 0.000000000000000000, 0.000000000000000000 ) ) ;
#29619=ADVANCED_FACE ( 'NONE', ( #41031 ), #41444, .F. ) ;
#29969=ORIENTED_EDGE ( 'NONE', *, *, #66020, .F. ) ;
#30003=FACE_OUTER_BOUND ( 'NONE', #61870, .T. ) ;
#30066=ORIENTED_EDGE ( 'NONE', *, *, #82328, .F. ) ;
#30091=CARTESIAN_POINT ( 'NONE',  ( 1.968503937007874072, 0.000000000000000000, 5.701968306260621233 ) ) ;
#30116=DIRECTION ( 'NONE',  ( -0.5773502691896305050, -0.5773502691896320593, 0.5773502691896145178 ) ) ;
#30305=ORIENTED_EDGE ( 'NONE', *, *, #22777, .F. ) ;
#30360=CIRCLE ( 'NONE', #70681, 0.01968503937007875723 ) ;
#30362=AXIS2_PLACEMENT_3D ( 'NONE', #37592, #11527, #37184 ) ;
#30529=EDGE_LOOP ( 'NONE', ( #68699, #5151, #42400, #66563 ) ) ;
#30596=CARTESIAN_POINT ( 'NONE',  ( 0.2642592750917004407, -0.1321325610835860920, 0.1571896754257856577 ) ) ;
#30627=CARTESIAN_POINT ( 'NONE',  ( 1.948818897637795367, 0.000000000000000000, 5.701968306260621233 ) ) ;
#30639=ORIENTED_EDGE ( 'NONE', *, *, #27779, .F. ) ;
#30642=ORIENTED_EDGE ( 'NONE', *, *, #70994, .F. ) ;
#30658=EDGE_CURVE ( 'NONE', #51820, #33736, #79481, .T. ) ;
#30716=DIRECTION ( 'NONE',  ( 0.000000000000000000, 0.000000000000000000, -1.000000000000000000 ) ) ;
#30829=CARTESIAN_POINT ( 'NONE',  ( -0.2896775404227472372, -0.05826908593210169962, 5.534257978450463966 ) ) ;
#30839=DIRECTION ( 'NONE',  ( 1.000000000000000000, 0.000000000000000000, -0.000000000000000000 ) ) ;
#30957=CARTESIAN_POINT ( 'NONE',  ( -0.2726377952755906220, 0.000000000000000000, 0.07874015748031495954 ) ) ;
#31040=VERTEX_POINT ( 'NONE', #44470 ) ;
#31079=AXIS2_PLACEMENT_3D ( 'NONE', #67009, #42141, #9342 ) ;
#31178=DIRECTION ( 'NONE',  ( 0.000000000000000000, 1.000000000000000000, 0.000000000000000000 ) ) ;
#31434=EDGE_LOOP ( 'NONE', ( #10528, #68909, #4909, #63947, #20579, #53699 ) ) ;
#31514=EDGE_CURVE ( 'NONE', #17617, #79188, #77320, .T. ) ;
#31518=EDGE_CURVE ( 'NONE', #51195, #31040, #53897, .T. ) ;
#31522=PLANE ( 'NONE',  #19673 ) ;
#31625=CARTESIAN_POINT ( 'NONE',  ( -0.2087913723976025926, 0.2087913723976025371, 0.1248231986745539646 ) ) ;
#31628=CARTESIAN_POINT ( 'NONE',  ( -0.2114133405073580496, -0.2061694042878472466, 0.1284558427095352229 ) ) ;
#31702=AXIS2_PLACEMENT_3D ( 'NONE', #72983, #8598, #60762 ) ;
#31798=AXIS2_PLACEMENT_3D ( 'NONE', #926, #14393, #47175 ) ;
#31960=EDGE_LOOP ( 'NONE', ( #71748, #28458, #46666, #292 ) ) ;
#32009=CARTESIAN_POINT ( 'NONE',  ( -0.2371566215357294172, 0.1759343135753352327, 5.725906639596367143 ) ) ;
#32060=ORIENTED_EDGE ( 'NONE', *, *, #67691, .F. ) ;
#32069=CARTESIAN_POINT ( 'NONE',  ( -0.2397245358942217408, -0.1724005034516534474, 5.660736073501680288 ) ) ;
#32183=LINE ( 'NONE', #65443, #78199 ) ;
#32253=VERTEX_POINT ( 'NONE', #76400 ) ;
#32509=AXIS2_PLACEMENT_3D ( 'NONE', #82158, #38760, #64437 ) ;
#32628=EDGE_CURVE ( 'NONE', #51375, #41668, #32183, .T. ) ;
#32727=AXIS2_PLACEMENT_3D ( 'NONE', #27782, #47128, #16004 ) ;
#32844=CARTESIAN_POINT ( 'NONE',  ( -0.2710150415003134139, 0.1175404812240907898, 5.835005246025586345 ) ) ;
#32883=PLANE ( 'NONE',  #23817 ) ;
#32885=CARTESIAN_POINT ( 'NONE',  ( -0.2142011206082509722, -0.2032823926810629067, 0.1316721176867485243 ) ) ;
#32979=CARTESIAN_POINT ( 'NONE',  ( 0.2917607380149856433, -0.04688787658492848953, 5.873221924710890107 ) ) ;
#33101=CARTESIAN_POINT ( 'NONE',  ( 0.1502491711592395529, -0.2549859370038549122, 0.1564451348283543985 ) ) ;
#33312=ORIENTED_EDGE ( 'NONE', *, *, #34017, .F. ) ;
#33316=CARTESIAN_POINT ( 'NONE',  ( -0.06463254593175619955, 0.06463254593175608853, -0.5032808398950130435 ) ) ;
#33436=EDGE_LOOP ( 'NONE', ( #82901, #40573, #71620, #26355 ) ) ;
#33531=ORIENTED_EDGE ( 'NONE', *, *, #70994, .T. ) ;
#33631=ORIENTED_EDGE ( 'NONE', *, *, #18554, .T. ) ;
#33684=CARTESIAN_POINT ( 'NONE',  ( -0.2396931915125568024, 0.1724440681141642395, 5.660914615074364775 ) ) ;
#33736=VERTEX_POINT ( 'NONE', #82209 ) ;
#34017=EDGE_CURVE ( 'NONE', #4461, #23692, #28430, .T. ) ;
#34101=B_SPLINE_CURVE_WITH_KNOTS ( 'NONE', 3,
 ( #36668, #24039, #49709, #72409, #20223, #71570, #21057, #53019, #32844, #1295, #19380, #52188, #13921, #77892, #14345, #32009, #65267, #20644, #14758, #33684, #1703, #8021, #7603, #57669, #63995, #31, #52606, #46297, #45872, #6336, #39577, #71992, #39150, #59346, #25684, #26945, #58513, #78313 ),
 .UNSPECIFIED., .F., .F.,
 ( 4, 2, 2, 2, 2, 2, 2, 2, 2, 2, 2, 2, 2, 2, 2, 2, 2, 2, 4 ),
 ( 7.825718265876660833E-19, 0.0009023223452592547779, 0.001804644690518508905, 0.002706967035777763791, 0.003609289381037018244, 0.004511611726296273564, 0.005413934071555528450, 0.006316256416814782469, 0.007218578762074037355, 0.008120901107333289640, 0.008572062279962877618, 0.009023223452592465596, 0.009925545797851638083, 0.01082786814311081230, 0.01173019048836998653, 0.01263251283362915901, 0.01353483517888833497, 0.01398599635151791254, 0.01443715752414749011 ),
 .UNSPECIFIED. ) ;
#34190=DIRECTION ( 'NONE',  ( 0.000000000000000000, 0.000000000000000000, -1.000000000000000000 ) ) ;
#34227=CARTESIAN_POINT ( 'NONE',  ( 0.2952755905511810774, 3.597759587968672259E-17, 5.524802951929911998 ) ) ;
#34230=EDGE_CURVE ( 'NONE', #51195, #67389, #1410, .T. ) ;
#34236=ADVANCED_FACE ( 'NONE', ( #42151 ), #2627, .F. ) ;
#34367=AXIS2_PLACEMENT_3D ( 'NONE', #835, #1256, #6711 ) ;
#34427=AXIS2_PLACEMENT_3D ( 'NONE', #67923, #80974, #30839 ) ;
#34447=ORIENTED_EDGE ( 'NONE', *, *, #8767, .F. ) ;
#34469=CIRCLE ( 'NONE', #10326, 0.1574803149606300579 ) ;
#34478=CARTESIAN_POINT ( 'NONE',  ( 0.2362214119660041856, 0.1771641016305865735, 5.695982005544458993 ) ) ;
#34525=CIRCLE ( 'NONE', #18362, 0.2952755905511810774 ) ;
#34548=CARTESIAN_POINT ( 'NONE',  ( 0.2396931915125568024, -0.1724440681141642395, 5.660914615074363887 ) ) ;
#34695=DIRECTION ( 'NONE',  ( 1.000000000000000000, 0.000000000000000000, 0.000000000000000000 ) ) ;
#34863=CARTESIAN_POINT ( 'NONE',  ( 0.1938976377952755792, -0.1938976377952756069, 0.07874015748031495954 ) ) ;
#34894=CARTESIAN_POINT ( 'NONE',  ( 0.2362186021731760011, 0.1771678480211529849, 5.713829339669467267 ) ) ;
#34952=CARTESIAN_POINT ( 'NONE',  ( 0.1938976377952755792, -0.1938976377952756069, -0.3740157480314971750 ) ) ;
#35103=ORIENTED_EDGE ( 'NONE', *, *, #50636, .T. ) ;
#35107=B_SPLINE_CURVE_WITH_KNOTS ( 'NONE', 3,
 ( #23405, #74357, #16701, #36042, #42755, #42341, #75182, #68039, #55382, #49072 ),
 .UNSPECIFIED., .F., .F.,
 ( 4, 2, 2, 2, 4 ),
 ( 1.301042606982605321E-18, 0.0007778963758021327198, 0.001555792751604264139, 0.002333689127406395666, 0.003111585503208526976 ),
 .UNSPECIFIED. ) ;
#35222=CARTESIAN_POINT ( 'NONE',  ( 1.948818897637795367, 0.000000000000000000, 5.701968306260621233 ) ) ;
#35302=CARTESIAN_POINT ( 'NONE',  ( 0.2843957880255121862, 0.07959014333740671576, 5.860354325783368346 ) ) ;
#35424=LINE ( 'NONE', #35840, #78148 ) ;
#35558=CIRCLE ( 'NONE', #66444, 0.2952755905511810774 ) ;
#35704=DIRECTION ( 'NONE',  ( -0.7071067811865333619, 0.000000000000000000, -0.7071067811865615615 ) ) ;
#35711=CARTESIAN_POINT ( 'NONE',  ( 0.2917302971764580977, 0.04706822171083047818, 5.873170128030150039 ) ) ;
#35756=LINE ( 'NONE', #23120, #7132 ) ;
#35793=ORIENTED_EDGE ( 'NONE', *, *, #67691, .T. ) ;
#35840=CARTESIAN_POINT ( 'NONE',  ( 0.1938976377952755792, 0.1938976377952755792, 0.1574803149606299191 ) ) ;
#35926=ORIENTED_EDGE ( 'NONE', *, *, #52272, .T. ) ;
#36036=EDGE_LOOP ( 'NONE', ( #45509, #27624, #71790, #11909, #72441, #42429 ) ) ;
#36042=CARTESIAN_POINT ( 'NONE',  ( 0.1830245018656607436, 0.2318981092368783414, 0.1465342031617538343 ) ) ;
#36073=B_SPLINE_CURVE_WITH_KNOTS ( 'NONE', 3,
 ( #38574, #704, #33101, #77727, #57507, #25940, #64255, #19214, #8268, #51599 ),
 .UNSPECIFIED., .F., .F.,
 ( 4, 2, 2, 2, 4 ),
 ( 0.000000000000000000, 0.001551611299846697867, 0.002327416949770047885, 0.002715319774731723545, 0.003103222599693399204 ),
 .UNSPECIFIED. ) ;
#36189=ADVANCED_FACE ( 'NONE', ( #44710 ), #81826, .T. ) ;
#36201=B_SPLINE_CURVE_WITH_KNOTS ( 'NONE', 3,
 ( #1014, #54299, #73690, #32979, #60625, #8871, #26667, #26243, #38872, #28641, #45593, #40854, #13224, #58646, #51481, #20357, #71704, #15196, #66959, #34548, #9703, #77184, #19516, #60214, #64551, #21911, #6888, #2564, #77610, #41676, #15615, #28222, #2975, #53881, #79596, #587, #47573, #16030 ),
 .UNSPECIFIED., .F., .F.,
 ( 4, 2, 2, 2, 2, 2, 2, 2, 2, 2, 2, 2, 2, 2, 2, 2, 2, 2, 4 ),
 ( 7.825718265876660833E-19, 0.0009023223452592552115, 0.001804644690518509556, 0.002706967035777763358, 0.003609289381037017377, 0.004511611726296271829, 0.005413934071555525848, 0.006316256416814780734, 0.007218578762074035621, 0.008120901107333289640, 0.008572062279962875883, 0.009023223452592462127, 0.009925545797851638083, 0.01082786814311081057, 0.01173019048836998653, 0.01263251283362916075, 0.01353483517888833497, 0.01398599635151791427, 0.01443715752414749184 ),
 .UNSPECIFIED. ) ;
#36218=ORIENTED_EDGE ( 'NONE', *, *, #12655, .T. ) ;
#36365=VECTOR ( 'NONE', #11286, 39.37007874015748143 ) ;
#36436=DIRECTION ( 'NONE',  ( 0.000000000000000000, 0.000000000000000000, -1.000000000000000000 ) ) ;
#36447=CARTESIAN_POINT ( 'NONE',  ( -0.1990279662527743021, -0.1990279662527743021, 0.1112963449492364171 ) ) ;
#36523=DIRECTION ( 'NONE',  ( -1.000000000000000000, -0.000000000000000000, -0.000000000000000000 ) ) ;
#36633=EDGE_CURVE ( 'NONE', #43843, #22229, #12208, .T. ) ;
#36668=CARTESIAN_POINT ( 'NONE',  ( -0.2952755905511810774, -3.179810529374183920E-17, 5.879133660591329580 ) ) ;
#36672=CARTESIAN_POINT ( 'NONE',  ( 0.1938976377952755792, -0.1938976377952756069, 0.09542247959850379269 ) ) ;
#36729=CARTESIAN_POINT ( 'NONE',  ( -0.2373513483963055337, -0.1756490242921440736, 5.678081160219037749 ) ) ;
#36858=ORIENTED_EDGE ( 'NONE', *, *, #20829, .F. ) ;
#36884=EDGE_CURVE ( 'NONE', #2979, #28061, #72137, .T. ) ;
#36910=CARTESIAN_POINT ( 'NONE',  ( 0.2491186766705762723, -0.1588297147722000924, 0.1541304905092664712 ) ) ;
#36921=EDGE_LOOP ( 'NONE', ( #62118, #44856, #54729, #12730 ) ) ;
#36976=CARTESIAN_POINT ( 'NONE',  ( 0.2726377952755905665, 0.1133856558944469489, 0.1574803149606299191 ) ) ;
#37146=CARTESIAN_POINT ( 'NONE',  ( -0.2445717520902165876, -0.1654678116698105328, 5.638396876410332048 ) ) ;
#37159=DIRECTION ( 'NONE',  ( -0.000000000000000000, 0.000000000000000000, -1.000000000000000000 ) ) ;
#37184=DIRECTION ( 'NONE',  ( 0.000000000000000000, 0.000000000000000000, 1.000000000000000000 ) ) ;
#37209=ORIENTED_EDGE ( 'NONE', *, *, #18554, .F. ) ;
#37243=PRODUCT_DEFINITION ( 'UNKNOWN', '', #40964, #41947 ) ;
#37517=PRESENTATION_STYLE_ASSIGNMENT (( #12685 ) ) ;
#37592=CARTESIAN_POINT ( 'NONE',  ( 1.968503937007874072, 0.000000000000000000, 5.701968306260621233 ) ) ;
#37669=AXIS2_PLACEMENT_3D ( 'NONE', #66187, #73753, #34190 ) ;
#37805=CARTESIAN_POINT ( 'NONE',  ( 0.2199809220305531665, 0.1970133122064496867, 0.1374248322900813168 ) ) ;
#37918=ADVANCED_FACE ( 'NONE', ( #18496 ), #31522, .F. ) ;
#38110=EDGE_CURVE ( 'NONE', #79188, #78367, #22226, .T. ) ;
#38139=CARTESIAN_POINT ( 'NONE',  ( -1.968503937007874072, 0.000000000000000000, 5.544487991299990703 ) ) ;
#38344=( NAMED_UNIT ( * ) PLANE_ANGLE_UNIT ( ) SI_UNIT ( $, .RADIAN. ) );
#38428=DIRECTION ( 'NONE',  ( 0.000000000000000000, 0.000000000000000000, -1.000000000000000000 ) ) ;
#38555=CARTESIAN_POINT ( 'NONE',  ( -0.1938976377952756625, 0.1938976377952755792, 0.07874015748031495954 ) ) ;
#38574=CARTESIAN_POINT ( 'NONE',  ( 0.1133856558944468795, -0.2726377952755905665, 0.1574803149606299191 ) ) ;
#38601=EDGE_LOOP ( 'NONE', ( #24087, #21076, #33312 ) ) ;
#38669=ORIENTED_EDGE ( 'NONE', *, *, #61343, .T. ) ;
#38760=DIRECTION ( 'NONE',  ( 1.000000000000000000, 0.000000000000000000, -0.000000000000000000 ) ) ;
#38807=ORIENTED_EDGE ( 'NONE', *, *, #63898, .F. ) ;
#38836=CARTESIAN_POINT ( 'NONE',  ( -0.2318981092368783692, 0.1830245018656607436, 0.1465342031617538066 ) ) ;
#38843=LINE ( 'NONE', #58193, #11480 ) ;
#38872=CARTESIAN_POINT ( 'NONE',  ( 0.2710150415003133029, -0.1175404812240907343, 5.835005246025582792 ) ) ;
#38927=CYLINDRICAL_SURFACE ( 'NONE', #80147, 0.07874015748031495954 ) ;
#38964=EDGE_CURVE ( 'NONE', #73460, #28061, #34469, .T. ) ;
#39110=DIRECTION ( 'NONE',  ( -0.000000000000000000, -0.000000000000000000, -1.000000000000000000 ) ) ;
#39150=CARTESIAN_POINT ( 'NONE',  ( -0.2917579853797115930, 0.04689358074580359664, 5.530719428720964892 ) ) ;
#39319=ORIENTED_EDGE ( 'NONE', *, *, #10205, .F. ) ;
#39322=CLOSED_SHELL ( 'NONE', ( #52359, #70250, #36189, #55647, #62473, #59591, #34236, #69083, #6324, #37918, #22780, #9537, #77338, #25998, #77464, #2342, #22947, #26530, #18831, #64507, #29619, #39555, #4835, #22460, #11345, #7398, #72318, #14954, #70511, #69203, #20079, #43389 ) ) ;
#39346=AXIS2_PLACEMENT_3D ( 'NONE', #19494, #12777, #26220 ) ;
#39555=ADVANCED_FACE ( 'NONE', ( #39969 ), #58476, .F. ) ;
#39577=CARTESIAN_POINT ( 'NONE',  ( -0.2845256677560919489, 0.07972153265861246785, 5.543321648279010638 ) ) ;
#39628=CARTESIAN_POINT ( 'NONE',  ( 1.968503937007874072, 0.000000000000000000, 5.701968306260621233 ) ) ;
#39708=VECTOR ( 'NONE', #39110, 39.37007874015748143 ) ;
#39969=FACE_OUTER_BOUND ( 'NONE', #64908, .T. ) ;
#39994=CIRCLE ( 'NONE', #69275, 0.1574803149606300579 ) ;
#40039=ORIENTED_EDGE ( 'NONE', *, *, #44272, .T. ) ;
#40098=CARTESIAN_POINT ( 'NONE',  ( -0.2378425880835044470, 0.1752652180395699311, 0.1496354662858539464 ) ) ;
#40268=DIRECTION ( 'NONE',  ( 0.000000000000000000, 1.000000000000000000, -1.224646799147353207E-16 ) ) ;
#40284=LINE ( 'NONE', #12024, #45204 ) ;
#40312=DIRECTION ( 'NONE',  ( 0.000000000000000000, 1.000000000000000000, -1.224646799147353207E-16 ) ) ;
#40413=LINE ( 'NONE', #80803, #79739 ) ;
#40573=ORIENTED_EDGE ( 'NONE', *, *, #52272, .F. ) ;
#40589=SHAPE_DEFINITION_REPRESENTATION ( #41327, #61632 ) ;
#40729=EDGE_LOOP ( 'NONE', ( #76506, #17506, #50885, #14926 ) ) ;
#40781=CARTESIAN_POINT ( 'NONE',  ( 0.2917632292039851194, 0.04688088360317046316, 5.530710407408372831 ) ) ;
#40854=CARTESIAN_POINT ( 'NONE',  ( 0.2524317427257167790, -0.1533591454305971991, 5.791393970467345831 ) ) ;
#40964=PRODUCT_DEFINITION_FORMATION_WITH_SPECIFIED_SOURCE ( 'ANY', '', #70817, .NOT_KNOWN. ) ;
#40980=EDGE_CURVE ( 'NONE', #64172, #70570, #65283, .T. ) ;
#41031=FACE_OUTER_BOUND ( 'NONE', #36921, .T. ) ;
#41203=CARTESIAN_POINT ( 'NONE',  ( 0.2371198560983137360, 0.1759840215932894636, 5.725591907046406526 ) ) ;
#41313=VECTOR ( 'NONE', #1334, 39.37007874015748854 ) ;
#41327=PRODUCT_DEFINITION_SHAPE ( 'NONE', 'NONE',  #37243 ) ;
#41329=PLANE ( 'NONE',  #31079 ) ;
#41444=PLANE ( 'NONE',  #59310 ) ;
#41601=DIRECTION ( 'NONE',  ( 0.000000000000000000, 0.000000000000000000, -1.000000000000000000 ) ) ;
#41609=CARTESIAN_POINT ( 'NONE',  ( 0.2380158072512373602, 0.1747520019874606312, 5.672240063627637774 ) ) ;
#41661=DIRECTION ( 'NONE',  ( 1.000000000000000000, 8.805702923740138355E-17, -0.000000000000000000 ) ) ;
#41668=VERTEX_POINT ( 'NONE', #66539 ) ;
#41676=CARTESIAN_POINT ( 'NONE',  ( 0.2814773692359251456, -0.08976595949324575607, 5.548806511850565393 ) ) ;
#41696=ORIENTED_EDGE ( 'NONE', *, *, #55977, .T. ) ;
#41699=EDGE_LOOP ( 'NONE', ( #58884, #61041 ) ) ;
#41759=EDGE_CURVE ( 'NONE', #41668, #51820, #36201, .T. ) ;
#41763=FACE_OUTER_BOUND ( 'NONE', #54617, .T. ) ;
#41879=CARTESIAN_POINT ( 'NONE',  ( -0.1228903193441467367, -0.2686849592492765448, 0.1574803149606299191 ) ) ;
#41947=PRODUCT_DEFINITION_CONTEXT ( 'detailed design', #6766, 'design' ) ;
#41962=CARTESIAN_POINT ( 'NONE',  ( 0.1938976377952755792, -0.1938976377952756069, 0.07874015748031495954 ) ) ;
#41991=ORIENTED_EDGE ( 'NONE', *, *, #13707, .F. ) ;
#42141=DIRECTION ( 'NONE',  ( -8.805702923740138355E-17, 1.000000000000000000, 0.000000000000000000 ) ) ;
#42148=CYLINDRICAL_SURFACE ( 'NONE', #2323, 0.1771653543307088186 ) ;
#42151=FACE_OUTER_BOUND ( 'NONE', #38601, .T. ) ;
#42182=CARTESIAN_POINT ( 'NONE',  ( -0.2952755905511810774, 0.000000000000000000, 0.1574803149606299191 ) ) ;
#42224=ORIENTED_EDGE ( 'NONE', *, *, #36884, .F. ) ;
#42341=CARTESIAN_POINT ( 'NONE',  ( 0.1588297147722000091, 0.2491186766705762723, 0.1541304905092664712 ) ) ;
#42400=ORIENTED_EDGE ( 'NONE', *, *, #20715, .T. ) ;
#42429=ORIENTED_EDGE ( 'NONE', *, *, #57908, .F. ) ;
#42432=ORIENTED_EDGE ( 'NONE', *, *, #49711, .T. ) ;
#42638=ORIENTED_EDGE ( 'NONE', *, *, #20291, .F. ) ;
#42706=CARTESIAN_POINT ( 'NONE',  ( -0.1830245018656607436, -0.2318981092368783414, 0.1465342031617537788 ) ) ;
#42716=DIRECTION ( 'NONE',  ( 0.000000000000000000, 0.000000000000000000, -1.000000000000000000 ) ) ;
#42755=CARTESIAN_POINT ( 'NONE',  ( 0.1752652180395700143, 0.2378425880835044193, 0.1496354662858539741 ) ) ;
#42809=ORIENTED_EDGE ( 'NONE', *, *, #16767, .T. ) ;
#42865=CARTESIAN_POINT ( 'NONE',  ( 0.1133856558944468795, -0.2726377952755905665, 0.1574803149606299191 ) ) ;
#42893=VERTEX_POINT ( 'NONE', #25668 ) ;
#43037=CARTESIAN_POINT ( 'NONE',  ( 0.000000000000000000, 0.000000000000000000, 6.062992125984251857 ) ) ;
#43096=VERTEX_POINT ( 'NONE', #61639 ) ;
#43204=CARTESIAN_POINT ( 'NONE',  ( 0.2544983382031790753, -0.1500752278769513504, 0.1555222293686583102 ) ) ;
#43213=ORIENTED_EDGE ( 'NONE', *, *, #9570, .F. ) ;
#43228=EDGE_LOOP ( 'NONE', ( #35103, #32060, #40039, #15413, #73270, #15533 ) ) ;
#43389=ADVANCED_FACE ( 'NONE', ( #75927 ), #13835, .T. ) ;
#43430=ORIENTED_EDGE ( 'NONE', *, *, #43522, .F. ) ;
#43443=CARTESIAN_POINT ( 'NONE',  ( -0.2952755905511810774, -0.01200600163628312393, 5.879133660591331356 ) ) ;
#43522=EDGE_CURVE ( 'NONE', #78156, #895, #366, .T. ) ;
#43702=TOROIDAL_SURFACE ( 'NONE', #34367, 0.1574803149606295860, 0.01968503937007873988 ) ;
#43827=DIRECTION ( 'NONE',  ( 0.000000000000000000, 0.000000000000000000, 1.000000000000000000 ) ) ;
#43843=VERTEX_POINT ( 'NONE', #67210 ) ;
#43853=CARTESIAN_POINT ( 'NONE',  ( -0.2746809754671077908, -0.1088096450009771038, 5.561685372298315500 ) ) ;
#43989=CIRCLE ( 'NONE', #77604, 0.1771653543307088186 ) ;
#44109=CARTESIAN_POINT ( 'NONE',  ( 0.2726377952755905665, 0.1133856558944469489, 0.1574803149606299191 ) ) ;
#44266=CARTESIAN_POINT ( 'NONE',  ( -0.2430399508222474692, -0.1677739497468299645, 5.760042173782278674 ) ) ;
#44272=EDGE_CURVE ( 'NONE', #28560, #64172, #2222, .T. ) ;
#44310=DIRECTION ( 'NONE',  ( 1.000000000000000000, 0.000000000000000000, 0.000000000000000000 ) ) ;
#44470=CARTESIAN_POINT ( 'NONE',  ( -1.948818897637795367, 0.000000000000000000, 5.879133660591329580 ) ) ;
#44479=ORIENTED_EDGE ( 'NONE', *, *, #2516, .T. ) ;
#44710=FACE_OUTER_BOUND ( 'NONE', #22336, .T. ) ;
#44775=ORIENTED_EDGE ( 'NONE', *, *, #17090, .T. ) ;
#44796=DIRECTION ( 'NONE',  ( 1.000000000000000000, 0.000000000000000000, -0.000000000000000000 ) ) ;
#44856=ORIENTED_EDGE ( 'NONE', *, *, #17268, .F. ) ;
#44931=DIRECTION ( 'NONE',  ( -1.000000000000000000, 0.000000000000000000, 0.000000000000000000 ) ) ;
#45070=LINE ( 'NONE', #33316, #41313 ) ;
#45072=CARTESIAN_POINT ( 'NONE',  ( -0.2379288306351265425, -0.1751536117528151026, 0.1496817530000226215 ) ) ;
#45094=CARTESIAN_POINT ( 'NONE',  ( -0.2364516566766633465, -0.1768582946180018434, 5.689955017551601379 ) ) ;
#45125=AXIS2_PLACEMENT_3D ( 'NONE', #18056, #25168, #62664 ) ;
#45128=DIRECTION ( 'NONE',  ( 0.000000000000000000, 0.000000000000000000, 1.000000000000000000 ) ) ;
#45204=VECTOR ( 'NONE', #11204, 39.37007874015748143 ) ;
#45222=DIRECTION ( 'NONE',  ( 0.000000000000000000, 0.000000000000000000, -1.000000000000000000 ) ) ;
#45243=VECTOR ( 'NONE', #61618, 39.37007874015748143 ) ;
#45303=VECTOR ( 'NONE', #23517, 39.37007874015748143 ) ;
#45494=FACE_OUTER_BOUND ( 'NONE', #54288, .T. ) ;
#45506=ORIENTED_EDGE ( 'NONE', *, *, #19638, .F. ) ;
#45509=ORIENTED_EDGE ( 'NONE', *, *, #17090, .F. ) ;
#45537=CARTESIAN_POINT ( 'NONE',  ( -0.000000000000000000, 0.1742125984251973736, -0.3937007874015748254 ) ) ;
#45593=CARTESIAN_POINT ( 'NONE',  ( 0.2596916824146294211, -0.1407161764240515978, 5.810203857714901332 ) ) ;
#45688=DIRECTION ( 'NONE',  ( -0.000000000000000000, 1.000000000000000000, -0.000000000000000000 ) ) ;
#45834=VECTOR ( 'NONE', #20497, 39.37007874015748143 ) ;
#45872=CARTESIAN_POINT ( 'NONE',  ( -0.2747679750349199534, 0.1085817515558208796, 5.561517368279697671 ) ) ;
#45888=EDGE_LOOP ( 'NONE', ( #33631, #3622 ) ) ;
#46189=LINE ( 'NONE', #70200, #21130 ) ;
#46230=ORIENTED_EDGE ( 'NONE', *, *, #60899, .T. ) ;
#46297=CARTESIAN_POINT ( 'NONE',  ( -0.2710655044954047299, 0.1174279065223611113, 5.568826803765084321 ) ) ;
#46472=ORIENTED_EDGE ( 'NONE', *, *, #23260, .T. ) ;
#46482=CARTESIAN_POINT ( 'NONE',  ( -0.1938976377952756625, -0.1938976377952756625, -0.3740157480314971750 ) ) ;
#46512=ORIENTED_EDGE ( 'NONE', *, *, #18921, .F. ) ;
#46577=ORIENTED_EDGE ( 'NONE', *, *, #25498, .F. ) ;
#46650=ORIENTED_EDGE ( 'NONE', *, *, #81093, .T. ) ;
#46666=ORIENTED_EDGE ( 'NONE', *, *, #55977, .F. ) ;
#46734=EDGE_LOOP ( 'NONE', ( #9116, #4494 ) ) ;
#46811=CARTESIAN_POINT ( 'NONE',  ( 0.000000000000000000, 0.000000000000000000, 0.1574803149606299191 ) ) ;
#46877=PLANE ( 'NONE',  #57220 ) ;
#46889=PRODUCT_CONTEXT ( 'NONE', #13801, 'mechanical' ) ;
#47017=EDGE_CURVE ( 'NONE', #32253, #5025, #60202, .T. ) ;
#47086=CARTESIAN_POINT ( 'NONE',  ( 0.2845468109762787079, 0.07963338598832106485, 5.543284456214099265 ) ) ;
#47090=ORIENTED_EDGE ( 'NONE', *, *, #81662, .F. ) ;
#47128=DIRECTION ( 'NONE',  ( 1.000000000000000000, 0.000000000000000000, 0.000000000000000000 ) ) ;
#47138=DIRECTION ( 'NONE',  ( 0.000000000000000000, 0.000000000000000000, 1.000000000000000000 ) ) ;
#47175=DIRECTION ( 'NONE',  ( 0.000000000000000000, 0.000000000000000000, -1.000000000000000000 ) ) ;
#47233=CARTESIAN_POINT ( 'NONE',  ( 0.1133856558944469489, 0.2726377952755905665, 0.1574803149606299191 ) ) ;
#47374=VERTEX_POINT ( 'NONE', #49214 ) ;
#47501=CARTESIAN_POINT ( 'NONE',  ( 0.2896775404227472372, 0.05826908593210169962, 5.534257978450463966 ) ) ;
#47573=CARTESIAN_POINT ( 'NONE',  ( 0.2952755905511810219, -0.005994596871347899689, 5.524802951929911110 ) ) ;
#47625=FACE_OUTER_BOUND ( 'NONE', #78751, .T. ) ;
#47669=CARTESIAN_POINT ( 'NONE',  ( -0.1938976377952756625, -0.1938976377952756625, -0.3740157480314971750 ) ) ;
#47706=EDGE_LOOP ( 'NONE', ( #7425, #60429, #17778, #72360 ) ) ;
#47778=CARTESIAN_POINT ( 'NONE',  ( -0.1588297147722000369, -0.2491186766705763000, 0.1541304905092664712 ) ) ;
#47802=EDGE_CURVE ( 'NONE', #78367, #28560, #50443, .T. ) ;
#48130=DIRECTION ( 'NONE',  ( -1.000000000000000000, -8.805702923740138355E-17, 0.000000000000000000 ) ) ;
#48328=CARTESIAN_POINT ( 'NONE',  ( 0.2397245358942217408, 0.1724005034516534474, 5.660736073501680288 ) ) ;
#48457=FACE_OUTER_BOUND ( 'NONE', #82313, .T. ) ;
#48492=LINE ( 'NONE', #47669, #19338 ) ;
#48497=ORIENTED_EDGE ( 'NONE', *, *, #50925, .T. ) ;
#48640=EDGE_LOOP ( 'NONE', ( #63649, #14997 ) ) ;
#48664=DIRECTION ( 'NONE',  ( -1.000000000000000000, -0.000000000000000000, -0.000000000000000000 ) ) ;
#48788=DIRECTION ( 'NONE',  ( -0.000000000000000000, -0.000000000000000000, -1.000000000000000000 ) ) ;
#48952=ORIENTED_EDGE ( 'NONE', *, *, #20829, .T. ) ;
#49021=AXIS2_PLACEMENT_3D ( 'NONE', #9530, #36436, #68843 ) ;
#49072=CARTESIAN_POINT ( 'NONE',  ( 0.1133856558944469489, 0.2726377952755905665, 0.1574803149606299191 ) ) ;
#49214=CARTESIAN_POINT ( 'NONE',  ( 0.2087913723976025926, 0.2087913723976026203, 0.1248231986745541033 ) ) ;
#49224=VECTOR ( 'NONE', #58277, 39.37007874015748143 ) ;
#49425=ORIENTED_EDGE ( 'NONE', *, *, #20715, .F. ) ;
#49709=CARTESIAN_POINT ( 'NONE',  ( -0.2945438235763074841, 0.02380624310431164042, 5.877921531841205471 ) ) ;
#49711=EDGE_CURVE ( 'NONE', #78367, #5025, #26487, .T. ) ;
#49749=B_SPLINE_CURVE_WITH_KNOTS ( 'NONE', 3,
 ( #25504, #17571, #11252, #62586, #4928, #36910, #43204, #30596, #50764, #18394 ),
 .UNSPECIFIED., .F., .F.,
 ( 4, 2, 2, 2, 4 ),
 ( 0.000000000000000000, 0.0007778963758021317440, 0.001555792751604263488, 0.002333689127406395232, 0.003111585503208526976 ),
 .UNSPECIFIED. ) ;
#49770=CARTESIAN_POINT ( 'NONE',  ( -0.2813683484248658551, -0.08970734455876072655, 5.854851642268653400 ) ) ;
#49780=PLANE ( 'NONE',  #34427 ) ;
#49799=DIRECTION ( 'NONE',  ( -0.000000000000000000, -0.000000000000000000, -1.000000000000000000 ) ) ;
#50172=EDGE_CURVE ( 'NONE', #51375, #2979, #52917, .T. ) ;
#50181=CARTESIAN_POINT ( 'NONE',  ( -0.2431881074996896375, -0.1674863405202415556, 5.643916622257989957 ) ) ;
#50213=EDGE_CURVE ( 'NONE', #895, #74332, #17602, .T. ) ;
#50386=CIRCLE ( 'NONE', #49021, 0.2952755905511810774 ) ;
#50443=LINE ( 'NONE', #19294, #21944 ) ;
#50555=ORIENTED_EDGE ( 'NONE', *, *, #19718, .T. ) ;
#50562=CARTESIAN_POINT ( 'NONE',  ( 0.000000000000000000, 0.000000000000000000, 0.1574803149606299191 ) ) ;
#50636=EDGE_CURVE ( 'NONE', #43843, #17617, #25166, .T. ) ;
#50658=AXIS2_PLACEMENT_3D ( 'NONE', #43037, #54016, #79727 ) ;
#50764=CARTESIAN_POINT ( 'NONE',  ( 0.2686849592492765448, -0.1228903193441468061, 0.1574803149606299191 ) ) ;
#50771=AXIS2_PLACEMENT_3D ( 'NONE', #22722, #3369, #41661 ) ;
#50837=CARTESIAN_POINT ( 'NONE',  ( -1.948818897637795367, 0.000000000000000000, 5.544487991299990703 ) ) ;
#50885=ORIENTED_EDGE ( 'NONE', *, *, #70415, .T. ) ;
#50925=EDGE_CURVE ( 'NONE', #66357, #43843, #3455, .T. ) ;
#50994=CARTESIAN_POINT ( 'NONE',  ( -0.2710308418177483358, -0.1175056764482960703, 5.568898341878665725 ) ) ;
#51195=VERTEX_POINT ( 'NONE', #66924 ) ;
#51375=VERTEX_POINT ( 'NONE', #61413 ) ;
#51409=CARTESIAN_POINT ( 'NONE',  ( -0.2635274766024540694, -0.1334916279589803412, 5.819004606509202482 ) ) ;
#51448=CIRCLE ( 'NONE', #15207, 0.1574803149606300579 ) ;
#51481=CARTESIAN_POINT ( 'NONE',  ( 0.2405786259268995197, -0.1712252042737591184, 5.748956133594166573 ) ) ;
#51520=VECTOR ( 'NONE', #35704, 39.37007874015748854 ) ;
#51530=FACE_OUTER_BOUND ( 'NONE', #31960, .T. ) ;
#51599=CARTESIAN_POINT ( 'NONE',  ( 0.2087913723976025926, -0.2087913723976025926, 0.1248231986745540617 ) ) ;
#51820=VERTEX_POINT ( 'NONE', #34227 ) ;
#51839=ORIENTED_EDGE ( 'NONE', *, *, #13707, .T. ) ;
#51869=CARTESIAN_POINT ( 'NONE',  ( -0.2087913723976025926, 0.2087913723976025371, 0.1248231986745539646 ) ) ;
#51956=ORIENTED_EDGE ( 'NONE', *, *, #31518, .T. ) ;
#52188=CARTESIAN_POINT ( 'NONE',  ( -0.2524317427257168345, 0.1533591454305971991, 5.791393970467346719 ) ) ;
#52227=CARTESIAN_POINT ( 'NONE',  ( -0.1990279662527743021, 0.1990279662527742188, 0.1112963449492363477 ) ) ;
#52230=CARTESIAN_POINT ( 'NONE',  ( -0.2087913723976026203, -0.2087913723976025926, 0.1248231986745540339 ) ) ;
#52238=DIRECTION ( 'NONE',  ( -1.000000000000000000, -0.000000000000000000, -0.000000000000000000 ) ) ;
#52272=EDGE_CURVE ( 'NONE', #11553, #5025, #48492, .T. ) ;
#52285=DIRECTION ( 'NONE',  ( 0.000000000000000000, 0.000000000000000000, 1.000000000000000000 ) ) ;
#52318=AXIS2_PLACEMENT_3D ( 'NONE', #24130, #49799, #8115 ) ;
#52359=ADVANCED_FACE ( 'NONE', ( #15712 ), #23366, .T. ) ;
#52367=FACE_OUTER_BOUND ( 'NONE', #17375, .T. ) ;
#52457=CARTESIAN_POINT ( 'NONE',  ( 0.1938976377952755792, 0.1938976377952755792, 0.07874015748031495954 ) ) ;
#52537=ORIENTED_EDGE ( 'NONE', *, *, #30658, .T. ) ;
#52606=CARTESIAN_POINT ( 'NONE',  ( -0.2635551335312363852, 0.1334335510540912706, 5.584872361112683592 ) ) ;
#52618=CARTESIAN_POINT ( 'NONE',  ( -0.1938976377952756625, 0.2726377952755905665, 0.1574803149606299191 ) ) ;
#52771=ORIENTED_EDGE ( 'NONE', *, *, #18921, .T. ) ;
#52917=CIRCLE ( 'NONE', #77081, 0.1771653543307088186 ) ;
#52953=VERTEX_POINT ( 'NONE', #4204 ) ;
#53019=CARTESIAN_POINT ( 'NONE',  ( -0.2746814661183892281, 0.1088119808354341828, 5.842252906343563978 ) ) ;
#53031=DIRECTION ( 'NONE',  ( 1.000000000000000000, 0.000000000000000000, 0.000000000000000000 ) ) ;
#53035=AXIS2_PLACEMENT_3D ( 'NONE', #39628, #52238, #26155 ) ;
#53118=DIRECTION ( 'NONE',  ( 1.000000000000000000, 0.000000000000000000, 0.000000000000000000 ) ) ;
#53148=VECTOR ( 'NONE', #30116, 39.37007874015748854 ) ;
#53187=DIRECTION ( 'NONE',  ( 0.000000000000000000, 1.000000000000000000, -0.000000000000000000 ) ) ;
#53246=AXIS2_PLACEMENT_3D ( 'NONE', #8723, #60887, #60062 ) ;
#53270=AXIS2_PLACEMENT_3D ( 'NONE', #70922, #7785, #44796 ) ;
#53510=LINE ( 'NONE', #29088, #55847 ) ;
#53601=EDGE_LOOP ( 'NONE', ( #43213, #9312, #42432, #50555 ) ) ;
#53699=ORIENTED_EDGE ( 'NONE', *, *, #25885, .F. ) ;
#53765=CARTESIAN_POINT ( 'NONE',  ( -0.1133856558944469489, 0.2726377952755905665, 0.1574803149606299191 ) ) ;
#53768=DIRECTION ( 'NONE',  ( -0.000000000000000000, -0.000000000000000000, -1.000000000000000000 ) ) ;
#53810=CARTESIAN_POINT ( 'NONE',  ( 0.2635424796782920853, 0.1334565945130699871, 5.584901928512098657 ) ) ;
#53881=CARTESIAN_POINT ( 'NONE',  ( 0.2938400550950684975, -0.02965148040547824562, 5.527203440556594849 ) ) ;
#53897=CIRCLE ( 'NONE', #4163, 0.01968503937007875723 ) ;
#53945=DIRECTION ( 'NONE',  ( 1.000000000000000000, 0.000000000000000000, -0.000000000000000000 ) ) ;
#53985=ORIENTED_EDGE ( 'NONE', *, *, #61343, .F. ) ;
#54016=DIRECTION ( 'NONE',  ( -0.000000000000000000, -0.000000000000000000, -1.000000000000000000 ) ) ;
#54226=CARTESIAN_POINT ( 'NONE',  ( 0.2797625792873952855, 0.09458053269141719621, 5.851882566737993230 ) ) ;
#54288=EDGE_LOOP ( 'NONE', ( #30066, #44775 ) ) ;
#54299=CARTESIAN_POINT ( 'NONE',  ( 0.2952755905511811885, -0.01202990275164721873, 5.879133660591332244 ) ) ;
#54319=( BOUNDED_CURVE ( )  B_SPLINE_CURVE ( 3, ( #60475, #2826, #28487, #59224 ),
 .UNSPECIFIED., .F., .F. ) 
 B_SPLINE_CURVE_WITH_KNOTS ( ( 4, 4 ),
 ( 5.657991264764151040, 6.283185307179586232 ),
 .UNSPECIFIED. ) 
 CURVE ( )  GEOMETRIC_REPRESENTATION_ITEM ( )  RATIONAL_B_SPLINE_CURVE ( ( 1.000000000000000000, 0.9676920770090842172, 0.9676920770090842172, 1.000000000000000000 ) ) 
 REPRESENTATION_ITEM ( '' )  );
#54617=EDGE_LOOP ( 'NONE', ( #41991, #57930, #53985 ) ) ;
#54646=CARTESIAN_POINT ( 'NONE',  ( 0.2858256400101374384, 0.07430968296373897941, 5.862902060615214239 ) ) ;
#54729=ORIENTED_EDGE ( 'NONE', *, *, #21343, .T. ) ;
#54743=EDGE_LOOP ( 'NONE', ( #313, #33531, #37209, #42224 ) ) ;
#54801=LINE ( 'NONE', #10617, #19917 ) ;
#54861=CARTESIAN_POINT ( 'NONE',  ( -0.1938976377952756625, 0.1938976377952755792, 0.1574803149606299191 ) ) ;
#54923=CARTESIAN_POINT ( 'NONE',  ( -0.1321325610835860087, -0.2642592750917004407, 0.1571896754257856577 ) ) ;
#55053=CARTESIAN_POINT ( 'NONE',  ( 0.2746809754671078463, 0.1088096450009770899, 5.561685372298315500 ) ) ;
#55062=CARTESIAN_POINT ( 'NONE',  ( -0.1936066689571366572, 0.2229926280064455923, 0.1399704324547694501 ) ) ;
#55216=DIRECTION ( 'NONE',  ( 0.000000000000000000, 0.000000000000000000, 1.000000000000000000 ) ) ;
#55264=LINE ( 'NONE', #10678, #62594 ) ;
#55331=CARTESIAN_POINT ( 'NONE',  ( -0.2087913723976026203, -0.2087913723976025926, 0.1248231986745540339 ) ) ;
#55382=CARTESIAN_POINT ( 'NONE',  ( 0.1228903193441468061, 0.2686849592492765448, 0.1574803149606299191 ) ) ;
#55386=DIRECTION ( 'NONE',  ( 0.000000000000000000, 0.000000000000000000, 1.000000000000000000 ) ) ;
#55450=VERTEX_POINT ( 'NONE', #64045 ) ;
#55492=CARTESIAN_POINT ( 'NONE',  ( -0.1938976377952756625, 0.1938976377952755792, 0.1574803149606299191 ) ) ;
#55647=ADVANCED_FACE ( 'NONE', ( #71619 ), #1753, .T. ) ;
#55670=ORIENTED_EDGE ( 'NONE', *, *, #17268, .T. ) ;
#55729=VERTEX_POINT ( 'NONE', #19429 ) ;
#55847=VECTOR ( 'NONE', #8909, 39.37007874015748143 ) ;
#55964=DIRECTION ( 'NONE',  ( 0.000000000000000000, 0.000000000000000000, 1.000000000000000000 ) ) ;
#55977=EDGE_CURVE ( 'NONE', #18348, #55450, #29298, .T. ) ;
#56026=CARTESIAN_POINT ( 'NONE',  ( 0.1990279662527742466, -0.1990279662527742466, 0.1112963449492364726 ) ) ;
#56043=CARTESIAN_POINT ( 'NONE',  ( 0.1938976377952755792, -0.1938976377952756069, -0.3740157480314971750 ) ) ;
#56085=CARTESIAN_POINT ( 'NONE',  ( -0.2362214119660041856, -0.1771641016305865735, 5.695982005544458993 ) ) ;
#56144=EDGE_CURVE ( 'NONE', #74332, #77294, #50386, .T. ) ;
#56192=ORIENTED_EDGE ( 'NONE', *, *, #40980, .T. ) ;
#56194=CIRCLE ( 'NONE', #14532, 0.2755905511811031494 ) ;
#56335=FACE_OUTER_BOUND ( 'NONE', #10858, .T. ) ;
#56452=ADVANCED_BREP_SHAPE_REPRESENTATION ( '', ( #6682, #22098 ), #65183 ) ;
#56455=LENGTH_MEASURE_WITH_UNIT ( LENGTH_MEASURE( 0.02539999999999999897 ), #12270 );
#56494=CARTESIAN_POINT ( 'NONE',  ( -0.2407687881342162883, -0.1709459579824098019, 5.655073192166721441 ) ) ;
#56843=CARTESIAN_POINT ( 'NONE',  ( 0.1938976377952755792, -0.1938976377952756069, 0.07874015748031495954 ) ) ;
#56909=ORIENTED_EDGE ( 'NONE', *, *, #50213, .T. ) ;
#56947=CARTESIAN_POINT ( 'NONE',  ( 0.1938976377952755792, 0.1938976377952755792, -0.3740157480314971750 ) ) ;
#57148=DIRECTION ( 'NONE',  ( 0.000000000000000000, 0.000000000000000000, -1.000000000000000000 ) ) ;
#57179=CARTESIAN_POINT ( 'NONE',  ( 0.1938976377952755792, 0.1938976377952755792, 0.1574803149606299191 ) ) ;
#57220=AXIS2_PLACEMENT_3D ( 'NONE', #54861, #74658, #37159 ) ;
#57233=DIRECTION ( 'NONE',  ( 0.000000000000000000, 0.000000000000000000, 1.000000000000000000 ) ) ;
#57286=CARTESIAN_POINT ( 'NONE',  ( -0.1938976377952756902, 0.1938976377952756069, 0.09542247959850373717 ) ) ;
#57318=ORIENTED_EDGE ( 'NONE', *, *, #36633, .T. ) ;
#57438=( CONVERSION_BASED_UNIT ( 'INCH', #4873 ) LENGTH_UNIT ( ) NAMED_UNIT ( #63153 ) );
#57444=AXIS2_PLACEMENT_3D ( 'NONE', #50562, #43827, #69116 ) ;
#57507=CARTESIAN_POINT ( 'NONE',  ( 0.1829408352246091884, -0.2319625946588664833, 0.1465682319128800981 ) ) ;
#57517=ORIENTED_EDGE ( 'NONE', *, *, #63069, .F. ) ;
#57566=CARTESIAN_POINT ( 'NONE',  ( 0.2319625946588665111, 0.1829408352246091884, 0.1465682319128801259 ) ) ;
#57669=CARTESIAN_POINT ( 'NONE',  ( -0.2489951994332677276, 0.1588014424199898911, 5.622579823899913620 ) ) ;
#57690=FILL_AREA_STYLE_COLOUR ( '', #28125 ) ;
#57720=ORIENTED_EDGE ( 'NONE', *, *, #36884, .T. ) ;
#57730=CARTESIAN_POINT ( 'NONE',  ( -0.2814587350932031828, -0.08983405572796258898, 5.548838678696989213 ) ) ;
#57908=EDGE_CURVE ( 'NONE', #16375, #43096, #36073, .T. ) ;
#57930=ORIENTED_EDGE ( 'NONE', *, *, #22777, .T. ) ;
#57987=CARTESIAN_POINT ( 'NONE',  ( 0.000000000000000000, 0.000000000000000000, 0.1574803149606299191 ) ) ;
#58094=CARTESIAN_POINT ( 'NONE',  ( 0.000000000000000000, 0.000000000000000000, 6.062992125984251857 ) ) ;
#58181=CYLINDRICAL_SURFACE ( 'NONE', #52318, 0.2952755905511810774 ) ;
#58184=CARTESIAN_POINT ( 'NONE',  ( -0.2726377952755906220, 0.1133856558944467546, 0.1574803149606299191 ) ) ;
#58193=CARTESIAN_POINT ( 'NONE',  ( 1.968503937007874072, 2.169649841009086334E-17, 5.524802951929911998 ) ) ;
#58204=VECTOR ( 'NONE', #59779, 39.37007874015748143 ) ;
#58277=DIRECTION ( 'NONE',  ( 0.000000000000000000, -1.000000000000000000, 0.000000000000000000 ) ) ;
#58321=AXIS2_PLACEMENT_3D ( 'NONE', #10216, #29556, #67050 ) ;
#58351=ORIENTED_EDGE ( 'NONE', *, *, #8767, .T. ) ;
#58471=LINE ( 'NONE', #71111, #39708 ) ;
#58476=CYLINDRICAL_SURFACE ( 'NONE', #10390, 0.07874015748031495954 ) ;
#58504=VECTOR ( 'NONE', #31178, 39.37007874015748143 ) ;
#58513=CARTESIAN_POINT ( 'NONE',  ( -0.2952755905511810219, 0.005994596871347967343, 5.524802951929910222 ) ) ;
#58529=ORIENTED_EDGE ( 'NONE', *, *, #69225, .F. ) ;
#58560=PLANE ( 'NONE',  #31798 ) ;
#58646=CARTESIAN_POINT ( 'NONE',  ( 0.2431027332089026050, -0.1676825148875300264, 5.760293869191739802 ) ) ;
#58850=CARTESIAN_POINT ( 'NONE',  ( -0.1742125984251974291, 0.1742125984251973736, -0.3937007874015748254 ) ) ;
#58884=ORIENTED_EDGE ( 'NONE', *, *, #76145, .T. ) ;
#58961=DIRECTION ( 'NONE',  ( 0.000000000000000000, 0.000000000000000000, -1.000000000000000000 ) ) ;
#59037=CARTESIAN_POINT ( 'NONE',  ( -0.2642592750917004962, 0.1321325610835859254, 0.1571896754257856577 ) ) ;
#59224=CARTESIAN_POINT ( 'NONE',  ( 0.1938976377952755792, 0.1938976377952755792, 0.07874015748031495954 ) ) ;
#59310=AXIS2_PLACEMENT_3D ( 'NONE', #66717, #28812, #9876 ) ;
#59346=CARTESIAN_POINT ( 'NONE',  ( -0.2938400550950686085, 0.02965148040547831848, 5.527203440556597513 ) ) ;
#59576=DIRECTION ( 'NONE',  ( 0.7071067811865333619, 8.659560562354760295E-17, -0.7071067811865615615 ) ) ;
#59579=CIRCLE ( 'NONE', #32727, 0.1771653543307088186 ) ;
#59591=ADVANCED_FACE ( 'NONE', ( #30003 ), #17407, .T. ) ;
#59690=ORIENTED_EDGE ( 'NONE', *, *, #56144, .F. ) ;
#59779=DIRECTION ( 'NONE',  ( 0.5773502691896306160, -0.5773502691896320593, 0.5773502691896146288 ) ) ;
#59869=CARTESIAN_POINT ( 'NONE',  ( 0.1938976377952755792, 0.1938976377952755792, -0.3740157480314971750 ) ) ;
#59932=CYLINDRICAL_SURFACE ( 'NONE', #31702, 0.07874015748031495954 ) ;
#60062=DIRECTION ( 'NONE',  ( 1.000000000000000000, 0.000000000000000000, 0.000000000000000000 ) ) ;
#60144=CARTESIAN_POINT ( 'NONE',  ( 0.2445717520902165876, 0.1654678116698105328, 5.638396876410332048 ) ) ;
#60202=LINE ( 'NONE', #34952, #58204 ) ;
#60214=CARTESIAN_POINT ( 'NONE',  ( 0.2489951994332677832, -0.1588014424199898911, 5.622579823899912732 ) ) ;
#60429=ORIENTED_EDGE ( 'NONE', *, *, #31514, .T. ) ;
#60475=CARTESIAN_POINT ( 'NONE',  ( 0.2087913723976025926, 0.2087913723976026203, 0.1248231986745541033 ) ) ;
#60484=UNCERTAINTY_MEASURE_WITH_UNIT (LENGTH_MEASURE( 1.000000000000000082E-05 ), #6359, 'distance_accuracy_value', 'NONE');
#60556=CARTESIAN_POINT ( 'NONE',  ( 0.2407687881342162883, 0.1709459579824098019, 5.655073192166721441 ) ) ;
#60625=CARTESIAN_POINT ( 'NONE',  ( 0.2896728340831398740, -0.05829427551933642759, 5.869670624399382142 ) ) ;
#60762=DIRECTION ( 'NONE',  ( 8.805702923740139587E-17, -1.000000000000000000, 0.000000000000000000 ) ) ;
#60857=EDGE_LOOP ( 'NONE', ( #41696, #34447, #58529, #46577 ) ) ;
#60887=DIRECTION ( 'NONE',  ( 0.000000000000000000, 0.000000000000000000, -1.000000000000000000 ) ) ;
#60899=EDGE_CURVE ( 'NONE', #31040, #42893, #43989, .T. ) ;
#60964=CARTESIAN_POINT ( 'NONE',  ( 0.2524666497344155158, 0.1533018367440332486, 5.791491733107224427 ) ) ;
#61018=PLANE ( 'NONE',  #50771 ) ;
#61041=ORIENTED_EDGE ( 'NONE', *, *, #34230, .T. ) ;
#61240=CARTESIAN_POINT ( 'NONE',  ( -0.1500752278769512948, -0.2544983382031791308, 0.1555222293686583102 ) ) ;
#61343=EDGE_CURVE ( 'NONE', #33736, #16379, #68245, .T. ) ;
#61381=CARTESIAN_POINT ( 'NONE',  ( 0.2945219335573386332, 0.02405856270293458068, 5.877884953661865808 ) ) ;
#61413=CARTESIAN_POINT ( 'NONE',  ( 1.948818897637795367, 0.000000000000000000, 5.879133660591329580 ) ) ;
#61486=EDGE_CURVE ( 'NONE', #23692, #64172, #10882, .T. ) ;
#61494=CARTESIAN_POINT ( 'NONE',  ( -1.948818897637795367, 0.000000000000000000, 5.701968306260621233 ) ) ;
#61508=DIRECTION ( 'NONE',  ( -0.000000000000000000, -0.000000000000000000, -1.000000000000000000 ) ) ;
#61618=DIRECTION ( 'NONE',  ( 0.000000000000000000, -1.000000000000000000, 0.000000000000000000 ) ) ;
#61632=SHAPE_REPRESENTATION ( 'Chuck Key Tool', ( #22098 ), #65183 ) ;
#61639=CARTESIAN_POINT ( 'NONE',  ( 0.2087913723976025926, -0.2087913723976025926, 0.1248231986745540617 ) ) ;
#61870=EDGE_LOOP ( 'NONE', ( #25019, #77662, #49425, #52537, #38669, #63447, #15032, #36218, #48497, #57318, #44479, #42638, #20272, #30639 ) ) ;
#62118=ORIENTED_EDGE ( 'NONE', *, *, #69225, .T. ) ;
#62120=CARTESIAN_POINT ( 'NONE',  ( -0.1938976377952756625, -0.1938976377952756625, 0.07874015748031495954 ) ) ;
#62405=CARTESIAN_POINT ( 'NONE',  ( -0.2362186021731760566, -0.1771678480211530127, 5.713829339669470819 ) ) ;
#62473=ADVANCED_FACE ( 'NONE', ( #4217 ), #73588, .T. ) ;
#62532=ORIENTED_EDGE ( 'NONE', *, *, #81093, .F. ) ;
#62586=CARTESIAN_POINT ( 'NONE',  ( 0.2318981092368783414, -0.1830245018656607436, 0.1465342031617538066 ) ) ;
#62594=VECTOR ( 'NONE', #48130, 39.37007874015748143 ) ;
#62602=DIMENSIONAL_EXPONENTS ( 1.000000000000000000, 0.000000000000000000, 0.000000000000000000, 0.000000000000000000, 0.000000000000000000, 0.000000000000000000, 0.000000000000000000 ) ;
#62634=CARTESIAN_POINT ( 'NONE',  ( -0.2032823926810630732, 0.2142011206082509445, 0.1316721176867485799 ) ) ;
#62644=AXIS2_PLACEMENT_3D ( 'NONE', #50837, #5004, #57148 ) ;
#62664=DIRECTION ( 'NONE',  ( 0.000000000000000000, 0.000000000000000000, -1.000000000000000000 ) ) ;
#62702=ORIENTED_EDGE ( 'NONE', *, *, #12540, .T. ) ;
#62831=CARTESIAN_POINT ( 'NONE',  ( -0.2635424796782920853, -0.1334565945130699871, 5.584901928512098657 ) ) ;
#62959=DIRECTION ( 'NONE',  ( 1.000000000000000000, 0.000000000000000000, 0.000000000000000000 ) ) ;
#62980=CARTESIAN_POINT ( 'NONE',  ( -0.2952755905511810774, 0.000000000000000000, 6.043307086614173151 ) ) ;
#63066=LINE ( 'NONE', #55492, #45303 ) ;
#63069=EDGE_CURVE ( 'NONE', #52953, #31040, #54801, .T. ) ;
#63153=DIMENSIONAL_EXPONENTS ( 1.000000000000000000, 0.000000000000000000, 0.000000000000000000, 0.000000000000000000, 0.000000000000000000, 0.000000000000000000, 0.000000000000000000 ) ;
#63442=CARTESIAN_POINT ( 'NONE',  ( 0.2952755905511810774, 3.179810529374183920E-17, 5.879133660591329580 ) ) ;
#63447=ORIENTED_EDGE ( 'NONE', *, *, #70567, .T. ) ;
#63483=FACE_OUTER_BOUND ( 'NONE', #54743, .T. ) ;
#63621=CARTESIAN_POINT ( 'NONE',  ( -0.2549859370038549677, -0.1502491711592393864, 0.1564451348283543985 ) ) ;
#63649=ORIENTED_EDGE ( 'NONE', *, *, #63898, .T. ) ;
#63764=PLANE ( 'NONE',  #53270 ) ;
#63842=EDGE_LOOP ( 'NONE', ( #43430, #16579, #59690, #19239 ) ) ;
#63851=VECTOR ( 'NONE', #66789, 39.37007874015748854 ) ;
#63860=ORIENTED_EDGE ( 'NONE', *, *, #41759, .T. ) ;
#63891=CARTESIAN_POINT ( 'NONE',  ( 0.2549859370038549122, 0.1502491711592394974, 0.1564451348283543708 ) ) ;
#63897=DIRECTION ( 'NONE',  ( 1.000000000000000000, 0.000000000000000000, -0.000000000000000000 ) ) ;
#63898=EDGE_CURVE ( 'NONE', #895, #78156, #56194, .T. ) ;
#63947=ORIENTED_EDGE ( 'NONE', *, *, #50925, .F. ) ;
#63995=CARTESIAN_POINT ( 'NONE',  ( -0.2524772379609336315, 0.1532855601034649740, 5.612412912560979628 ) ) ;
#64019=FACE_OUTER_BOUND ( 'NONE', #31434, .T. ) ;
#64045=CARTESIAN_POINT ( 'NONE',  ( 0.1742125984251973736, 0.1742125984251973736, -0.3937007874015748254 ) ) ;
#64155=EDGE_CURVE ( 'NONE', #19415, #66357, #26955, .T. ) ;
#64172=VERTEX_POINT ( 'NONE', #72002 ) ;
#64255=CARTESIAN_POINT ( 'NONE',  ( 0.1970133122064497144, -0.2199809220305531665, 0.1374248322900813446 ) ) ;
#64312=DIRECTION ( 'NONE',  ( 0.000000000000000000, 1.224646799147351482E-16, 1.000000000000000000 ) ) ;
#64437=DIRECTION ( 'NONE',  ( 0.000000000000000000, 0.000000000000000000, -1.000000000000000000 ) ) ;
#64445=EDGE_LOOP ( 'NONE', ( #12084, #51956, #65622, #66256 ) ) ;
#64507=ADVANCED_FACE ( 'NONE', ( #15597 ), #61018, .F. ) ;
#64515=CARTESIAN_POINT ( 'NONE',  ( -0.2686849592492766003, 0.1228903193441466535, 0.1574803149606299191 ) ) ;
#64551=CARTESIAN_POINT ( 'NONE',  ( 0.2524772379609335204, -0.1532855601034649740, 5.612412912560978739 ) ) ;
#64601=DIRECTION ( 'NONE',  ( -0.7071067811865376918, 0.000000000000000000, 0.7071067811865573427 ) ) ;
#64729=DIRECTION ( 'NONE',  ( -0.000000000000000000, 1.000000000000000000, 0.000000000000000000 ) ) ;
#64908=EDGE_LOOP ( 'NONE', ( #45506, #28873, #16346, #27685, #30305, #29969 ) ) ;
#65011=VECTOR ( 'NONE', #65246, 39.37007874015748143 ) ;
#65017=VERTEX_POINT ( 'NONE', #58850 ) ;
#65183=( GEOMETRIC_REPRESENTATION_CONTEXT ( 3 ) GLOBAL_UNCERTAINTY_ASSIGNED_CONTEXT ( ( #25993 ) ) GLOBAL_UNIT_ASSIGNED_CONTEXT ( ( #57438, #81911, #24223 ) ) REPRESENTATION_CONTEXT ( 'NONE', 'WORKASPACE' ) );
#65224=FACE_OUTER_BOUND ( 'NONE', #1125, .T. ) ;
#65246=DIRECTION ( 'NONE',  ( -0.000000000000000000, -0.000000000000000000, -1.000000000000000000 ) ) ;
#65267=CARTESIAN_POINT ( 'NONE',  ( -0.2362235781738432072, 0.1771612133531280942, 5.714029142339813738 ) ) ;
#65283=B_SPLINE_CURVE_WITH_KNOTS ( 'NONE', 3,
 ( #55331, #10742, #66751, #42706, #3594, #47778, #61240, #54923, #41879, #80630 ),
 .UNSPECIFIED., .F., .F.,
 ( 4, 2, 2, 2, 4 ),
 ( 4.336808689942017736E-19, 0.0007778963758021331535, 0.001555792751604265873, 0.002333689127406398701, 0.003111585503208531313 ),
 .UNSPECIFIED. ) ;
#65307=DIRECTION ( 'NONE',  ( 1.000000000000000000, 0.000000000000000000, 0.000000000000000000 ) ) ;
#65371=CARTESIAN_POINT ( 'NONE',  ( -0.2140388612101736809, 0.2035438835850314210, 0.1320934087364890874 ) ) ;
#65415=AXIS2_PLACEMENT_3D ( 'NONE', #9022, #78068, #34695 ) ;
#65420=AXIS2_PLACEMENT_3D ( 'NONE', #21235, #77657, #45222 ) ;
#65443=CARTESIAN_POINT ( 'NONE',  ( 1.968503937007874072, 0.000000000000000000, 5.879133660591329580 ) ) ;
#65622=ORIENTED_EDGE ( 'NONE', *, *, #76445, .F. ) ;
#65764=AXIS2_PLACEMENT_3D ( 'NONE', #46811, #52285, #53118 ) ;
#66020=EDGE_CURVE ( 'NONE', #43096, #55729, #49749, .T. ) ;
#66187=CARTESIAN_POINT ( 'NONE',  ( -1.968503937007874072, 0.000000000000000000, 5.701968306260621233 ) ) ;
#66201=FACE_OUTER_BOUND ( 'NONE', #60857, .T. ) ;
#66256=ORIENTED_EDGE ( 'NONE', *, *, #70415, .F. ) ;
#66357=VERTEX_POINT ( 'NONE', #53765 ) ;
#66385=DIRECTION ( 'NONE',  ( 0.000000000000000000, 0.000000000000000000, -1.000000000000000000 ) ) ;
#66444=AXIS2_PLACEMENT_3D ( 'NONE', #81504, #55386, #62959 ) ;
#66467=CARTESIAN_POINT ( 'NONE',  ( 0.2490413359174502850, 0.1587297840844698882, 5.622433025490734870 ) ) ;
#66539=CARTESIAN_POINT ( 'NONE',  ( 0.2952755905511810774, 3.179810529374183920E-17, 5.879133660591329580 ) ) ;
#66557=FACE_OUTER_BOUND ( 'NONE', #45888, .T. ) ;
#66563=ORIENTED_EDGE ( 'NONE', *, *, #32628, .F. ) ;
#66717=CARTESIAN_POINT ( 'NONE',  ( -0.1938976377952756625, 0.1938976377952755792, -0.3740157480314971750 ) ) ;
#66747=EDGE_CURVE ( 'NONE', #78156, #77294, #72633, .T. ) ;
#66751=CARTESIAN_POINT ( 'NONE',  ( -0.1972978822260921805, -0.2198823481317033202, 0.1376690760605703556 ) ) ;
#66789=DIRECTION ( 'NONE',  ( -0.5773502691896310601, -0.5773502691896310601, -0.5773502691896149619 ) ) ;
#66924=CARTESIAN_POINT ( 'NONE',  ( -1.968503937007874072, 2.049113738730800541E-17, 5.859448621221250875 ) ) ;
#66950=ORIENTED_EDGE ( 'NONE', *, *, #41759, .F. ) ;
#66959=CARTESIAN_POINT ( 'NONE',  ( 0.2371319115525429566, -0.1759675087575592323, 5.678257627497695914 ) ) ;
#67009=CARTESIAN_POINT ( 'NONE',  ( -0.1938976377952756625, -0.1938976377952756625, 0.1574803149606299191 ) ) ;
#67050=DIRECTION ( 'NONE',  ( 0.000000000000000000, 0.000000000000000000, -1.000000000000000000 ) ) ;
#67210=CARTESIAN_POINT ( 'NONE',  ( -0.2087913723976025926, 0.2087913723976025371, 0.1248231986745539646 ) ) ;
#67382=VECTOR ( 'NONE', #53768, 39.37007874015748143 ) ;
#67389=VERTEX_POINT ( 'NONE', #38139 ) ;
#67557=AXIS2_PLACEMENT_3D ( 'NONE', #3894, #55216, #80103 ) ;
#67585=VECTOR ( 'NONE', #3225, 39.37007874015748143 ) ;
#67691=EDGE_CURVE ( 'NONE', #28560, #17617, #12896, .T. ) ;
#67923=CARTESIAN_POINT ( 'NONE',  ( 0.000000000000000000, 0.000000000000000000, 6.062992125984251857 ) ) ;
#68039=CARTESIAN_POINT ( 'NONE',  ( 0.1321325610835860920, 0.2642592750917004407, 0.1571896754257856577 ) ) ;
#68212=CARTESIAN_POINT ( 'NONE',  ( 0.000000000000000000, 0.000000000000000000, 6.062992125984251857 ) ) ;
#68241=DIRECTION ( 'NONE',  ( 0.000000000000000000, 0.000000000000000000, -1.000000000000000000 ) ) ;
#68245=CIRCLE ( 'NONE', #57444, 0.2952755905511810774 ) ;
#68699=ORIENTED_EDGE ( 'NONE', *, *, #50172, .T. ) ;
#68760=CARTESIAN_POINT ( 'NONE',  ( 0.000000000000000000, 0.000000000000000000, 0.1574803149606299191 ) ) ;
#68843=DIRECTION ( 'NONE',  ( 1.000000000000000000, 0.000000000000000000, 0.000000000000000000 ) ) ;
#68909=ORIENTED_EDGE ( 'NONE', *, *, #31514, .F. ) ;
#68925=EDGE_LOOP ( 'NONE', ( #36858, #35793, #42809, #62702 ) ) ;
#68975=CARTESIAN_POINT ( 'NONE',  ( 1.968503937007874072, 0.000000000000000000, 5.701968306260621233 ) ) ;
#69083=ADVANCED_FACE ( 'NONE', ( #45494 ), #32883, .F. ) ;
#69085=LINE ( 'NONE', #12665, #58504 ) ;
#69116=DIRECTION ( 'NONE',  ( 1.000000000000000000, 0.000000000000000000, 0.000000000000000000 ) ) ;
#69203=ADVANCED_FACE ( 'NONE', ( #7646 ), #6373, .F. ) ;
#69225=EDGE_CURVE ( 'NONE', #21842, #65017, #45070, .T. ) ;
#69275=AXIS2_PLACEMENT_3D ( 'NONE', #83053, #44310, #38428 ) ;
#69276=ORIENTED_EDGE ( 'NONE', *, *, #76445, .T. ) ;
#69299=CARTESIAN_POINT ( 'NONE',  ( 1.968503937007874072, 2.049113738730800541E-17, 5.859448621221250875 ) ) ;
#69440=B_SPLINE_CURVE_WITH_KNOTS ( 'NONE', 3,
 ( #44109, #19272, #63891, #12148, #57566, #75302, #37805, #5816, #75715, #83258 ),
 .UNSPECIFIED., .F., .F.,
 ( 4, 2, 2, 2, 4 ),
 ( 0.000000000000000000, 0.001551611299846697217, 0.002327416949770047885, 0.002715319774731722677, 0.003103222599693397903 ),
 .UNSPECIFIED. ) ;
#69556=CARTESIAN_POINT ( 'NONE',  ( -0.2843957880255121307, -0.07959014333740668801, 5.860354325783371010 ) ) ;
#69687=LINE ( 'NONE', #77240, #49224 ) ;
#69819=DIRECTION ( 'NONE',  ( -1.000000000000000000, -8.805702923740138355E-17, -0.000000000000000000 ) ) ;
#69957=CARTESIAN_POINT ( 'NONE',  ( -0.2747288752779720178, -0.1086799599621181001, 5.842342907282080944 ) ) ;
#69986=DIRECTION ( 'NONE',  ( 1.000000000000000000, 0.000000000000000000, 0.000000000000000000 ) ) ;
#70200=CARTESIAN_POINT ( 'NONE',  ( -0.1742125984251974291, -0.000000000000000000, -0.3937007874015748254 ) ) ;
#70250=ADVANCED_FACE ( 'NONE', ( #63483 ), #3525, .T. ) ;
#70345=CARTESIAN_POINT ( 'NONE',  ( -1.968503937007874072, 0.000000000000000000, 5.701968306260621233 ) ) ;
#70415=EDGE_CURVE ( 'NONE', #67389, #42893, #14293, .T. ) ;
#70511=ADVANCED_FACE ( 'NONE', ( #56335 ), #76537, .T. ) ;
#70567=EDGE_CURVE ( 'NONE', #16379, #47374, #69440, .T. ) ;
#70570=VERTEX_POINT ( 'NONE', #11325 ) ;
#70622=DIRECTION ( 'NONE',  ( 0.000000000000000000, 0.000000000000000000, 1.000000000000000000 ) ) ;
#70681=AXIS2_PLACEMENT_3D ( 'NONE', #20541, #40312, #64312 ) ;
#70775=CARTESIAN_POINT ( 'NONE',  ( -0.2319625946588664833, -0.1829408352246090774, 0.1465682319128800981 ) ) ;
#70798=CARTESIAN_POINT ( 'NONE',  ( -0.2945512653497797673, -0.02373080790438483051, 5.526002588227517442 ) ) ;
#70817=PRODUCT ( 'Chuck Key Tool', 'Chuck Key Tool', '', ( #46889 ) ) ;
#70860=AXIS2_PLACEMENT_3D ( 'NONE', #70345, #65307, #26575 ) ;
#70910=DIRECTION ( 'NONE',  ( -1.000000000000000000, -0.000000000000000000, -0.000000000000000000 ) ) ;
#70922=CARTESIAN_POINT ( 'NONE',  ( 0.000000000000000000, 0.000000000000000000, -0.3937007874015748254 ) ) ;
#70980=VECTOR ( 'NONE', #2127, 39.37007874015748143 ) ;
#70994=EDGE_CURVE ( 'NONE', #51375, #73460, #30360, .T. ) ;
#71111=CARTESIAN_POINT ( 'NONE',  ( -0.2952755905511810774, 0.000000000000000000, 6.062992125984251857 ) ) ;
#71193=CARTESIAN_POINT ( 'NONE',  ( -0.2726377952755906220, -0.1133856558944467546, 0.1574803149606299191 ) ) ;
#71260=DIRECTION ( 'NONE',  ( -1.000000000000000000, -0.000000000000000000, -0.000000000000000000 ) ) ;
#71341=DIRECTION ( 'NONE',  ( -0.000000000000000000, 1.000000000000000000, 0.000000000000000000 ) ) ;
#71534=DIRECTION ( 'NONE',  ( 0.000000000000000000, 0.000000000000000000, -1.000000000000000000 ) ) ;
#71570=CARTESIAN_POINT ( 'NONE',  ( -0.2845351084527214525, 0.07967650482972132853, 5.860631297047876664 ) ) ;
#71608=DIRECTION ( 'NONE',  ( 1.000000000000000000, 0.000000000000000000, -0.000000000000000000 ) ) ;
#71619=FACE_OUTER_BOUND ( 'NONE', #30529, .T. ) ;
#71620=ORIENTED_EDGE ( 'NONE', *, *, #21343, .F. ) ;
#71704=CARTESIAN_POINT ( 'NONE',  ( 0.2362235781738431795, -0.1771612133531280942, 5.714029142339813738 ) ) ;
#71748=ORIENTED_EDGE ( 'NONE', *, *, #47017, .F. ) ;
#71790=ORIENTED_EDGE ( 'NONE', *, *, #44272, .F. ) ;
#71956=DIRECTION ( 'NONE',  ( 0.000000000000000000, -1.000000000000000000, 0.000000000000000000 ) ) ;
#71992=CARTESIAN_POINT ( 'NONE',  ( -0.2896989933648237980, 0.05817964957694448519, 5.534220241493016168 ) ) ;
#72002=CARTESIAN_POINT ( 'NONE',  ( -0.2087913723976026203, -0.2087913723976025926, 0.1248231986745540339 ) ) ;
#72084=AXIS2_PLACEMENT_3D ( 'NONE', #68975, #82034, #70622 ) ;
#72137=CIRCLE ( 'NONE', #65420, 0.01968503937007875723 ) ;
#72318=ADVANCED_FACE ( 'NONE', ( #66557 ), #58560, .T. ) ;
#72360=ORIENTED_EDGE ( 'NONE', *, *, #25498, .T. ) ;
#72409=CARTESIAN_POINT ( 'NONE',  ( -0.2917607380149855878, 0.04688787658492848259, 5.873221924710888331 ) ) ;
#72441=ORIENTED_EDGE ( 'NONE', *, *, #19638, .T. ) ;
#72487=DIRECTION ( 'NONE',  ( 1.000000000000000000, 0.000000000000000000, 0.000000000000000000 ) ) ;
#72633=LINE ( 'NONE', #14576, #21125 ) ;
#72776=CARTESIAN_POINT ( 'NONE',  ( 0.2710308418177483358, 0.1175056764482960842, 5.568898341878665725 ) ) ;
#72887=DIRECTION ( 'NONE',  ( 1.000000000000000000, 0.000000000000000000, 0.000000000000000000 ) ) ;
#72983=CARTESIAN_POINT ( 'NONE',  ( 2.400767430980333376E-17, -0.2726377952755905665, 0.07874015748031495954 ) ) ;
#73194=CARTESIAN_POINT ( 'NONE',  ( 0.2489800900487909585, 0.1588251575432187424, 5.781310865041811908 ) ) ;
#73270=ORIENTED_EDGE ( 'NONE', *, *, #76295, .F. ) ;
#73360=PLANE ( 'NONE',  #67557 ) ;
#73460=VERTEX_POINT ( 'NONE', #69299 ) ;
#73588=CONICAL_SURFACE ( 'NONE', #14474, 0.2755905511811031494, 0.7853981633974284060 ) ;
#73589=DIRECTION ( 'NONE',  ( 0.000000000000000000, -0.000000000000000000, -1.000000000000000000 ) ) ;
#73690=CARTESIAN_POINT ( 'NONE',  ( 0.2945438235763075396, -0.02380624310431164736, 5.877921531841206360 ) ) ;
#73753=DIRECTION ( 'NONE',  ( -1.000000000000000000, -0.000000000000000000, -0.000000000000000000 ) ) ;
#74025=CARTESIAN_POINT ( 'NONE',  ( 0.2431881074996896375, 0.1674863405202415556, 5.643916622257989957 ) ) ;
#74071=MECHANICAL_DESIGN_GEOMETRIC_PRESENTATION_REPRESENTATION('',(#27010),#17590);
#74104=ORIENTED_EDGE ( 'NONE', *, *, #66020, .T. ) ;
#74179=DIRECTION ( 'NONE',  ( -1.000000000000000000, -0.000000000000000000, -0.000000000000000000 ) ) ;
#74239=FACE_OUTER_BOUND ( 'NONE', #48640, .T. ) ;
#74314=DIRECTION ( 'NONE',  ( 1.000000000000000000, 0.000000000000000000, 0.000000000000000000 ) ) ;
#74332=VERTEX_POINT ( 'NONE', #62980 ) ;
#74357=CARTESIAN_POINT ( 'NONE',  ( 0.2035438835850314487, 0.2140388612101737920, 0.1320934087364891707 ) ) ;
#74536=ORIENTED_EDGE ( 'NONE', *, *, #30658, .F. ) ;
#74658=DIRECTION ( 'NONE',  ( 1.000000000000000000, 0.000000000000000000, -0.000000000000000000 ) ) ;
#74870=CARTESIAN_POINT ( 'NONE',  ( -0.1502491711592395529, 0.2549859370038549122, 0.1564451348283543985 ) ) ;
#75182=CARTESIAN_POINT ( 'NONE',  ( 0.1500752278769513226, 0.2544983382031791308, 0.1555222293686583102 ) ) ;
#75302=CARTESIAN_POINT ( 'NONE',  ( 0.2229926280064457034, 0.1936066689571366295, 0.1399704324547694778 ) ) ;
#75410=CARTESIAN_POINT ( 'NONE',  ( 0.2087913723976025926, -0.2087913723976025926, 0.1248231986745540617 ) ) ;
#75470=CARTESIAN_POINT ( 'NONE',  ( -0.2952755905511810774, -0.01196537350834416848, 5.524802951929911110 ) ) ;
#75490=AXIS2_PLACEMENT_3D ( 'NONE', #17005, #26183, #19884 ) ;
#75675=CARTESIAN_POINT ( 'NONE',  ( -0.2755905511811031494, 0.000000000000000000, 6.062992125984251857 ) ) ;
#75715=CARTESIAN_POINT ( 'NONE',  ( 0.2114133405073579941, 0.2061694042878472466, 0.1284558427095351951 ) ) ;
#75876=CARTESIAN_POINT ( 'NONE',  ( -0.2710828156362889985, -0.1173918767474883551, 5.835147349599719035 ) ) ;
#75879=EDGE_CURVE ( 'NONE', #52953, #23282, #34101, .T. ) ;
#75927=FACE_OUTER_BOUND ( 'NONE', #40729, .T. ) ;
#76000=( LENGTH_UNIT ( ) NAMED_UNIT ( * ) SI_UNIT ( $, .METRE. ) );
#76008=DIRECTION ( 'NONE',  ( 0.000000000000000000, 0.000000000000000000, 1.000000000000000000 ) ) ;
#76145=EDGE_CURVE ( 'NONE', #67389, #51195, #51448, .T. ) ;
#76295=EDGE_CURVE ( 'NONE', #22229, #23692, #40413, .T. ) ;
#76400=CARTESIAN_POINT ( 'NONE',  ( 0.1742125984251973736, -0.1742125984251973736, -0.3937007874015748254 ) ) ;
#76404=EDGE_CURVE ( 'NONE', #77294, #41668, #35756, .T. ) ;
#76445=EDGE_CURVE ( 'NONE', #42893, #31040, #59579, .T. ) ;
#76506=ORIENTED_EDGE ( 'NONE', *, *, #31518, .F. ) ;
#76537=CYLINDRICAL_SURFACE ( 'NONE', #72084, 0.1771653543307088186 ) ;
#76692=CARTESIAN_POINT ( 'NONE',  ( -0.2952755905511810774, -3.179810529374183920E-17, 5.879133660591329580 ) ) ;
#77081=AXIS2_PLACEMENT_3D ( 'NONE', #30627, #36523, #41601 ) ;
#77111=CARTESIAN_POINT ( 'NONE',  ( -0.2489800900487910418, -0.1588251575432186868, 5.781310865041811020 ) ) ;
#77184=CARTESIAN_POINT ( 'NONE',  ( 0.2431769186048377551, -0.1675026378872651045, 5.643961825897843454 ) ) ;
#77233=PLANE ( 'NONE',  #23718 ) ;
#77240=CARTESIAN_POINT ( 'NONE',  ( 0.1742125984251973736, -0.000000000000000000, -0.3937007874015748254 ) ) ;
#77294=VERTEX_POINT ( 'NONE', #14245 ) ;
#77320=LINE ( 'NONE', #52457, #45834 ) ;
#77338=ADVANCED_FACE ( 'NONE', ( #25586 ), #20127, .F. ) ;
#77464=ADVANCED_FACE ( 'NONE', ( #20547 ), #19702, .F. ) ;
#77604=AXIS2_PLACEMENT_3D ( 'NONE', #61494, #72887, #68241 ) ;
#77610=CARTESIAN_POINT ( 'NONE',  ( 0.2747679750349198979, -0.1085817515558208796, 5.561517368279697671 ) ) ;
#77657=DIRECTION ( 'NONE',  ( 0.000000000000000000, -1.000000000000000000, 0.000000000000000000 ) ) ;
#77662=ORIENTED_EDGE ( 'NONE', *, *, #76404, .T. ) ;
#77727=CARTESIAN_POINT ( 'NONE',  ( 0.1751536117528151582, -0.2379288306351265148, 0.1496817530000226215 ) ) ;
#77892=CARTESIAN_POINT ( 'NONE',  ( -0.2431027332089026605, 0.1676825148875300264, 5.760293869191740690 ) ) ;
#78068=DIRECTION ( 'NONE',  ( 0.000000000000000000, 0.000000000000000000, 1.000000000000000000 ) ) ;
#78148=VECTOR ( 'NONE', #61508, 39.37007874015748143 ) ;
#78156=VERTEX_POINT ( 'NONE', #21375 ) ;
#78199=VECTOR ( 'NONE', #70910, 39.37007874015748143 ) ;
#78313=CARTESIAN_POINT ( 'NONE',  ( -0.2952755905511810774, 1.832348042626885162E-19, 5.524802951929911998 ) ) ;
#78345=ORIENTED_EDGE ( 'NONE', *, *, #57908, .T. ) ;
#78354=CARTESIAN_POINT ( 'NONE',  ( -0.2647380121165202049, -0.1323808228461570424, 0.1574803149606299746 ) ) ;
#78367=VERTEX_POINT ( 'NONE', #41962 ) ;
#78751=EDGE_LOOP ( 'NONE', ( #81573, #12694, #48952, #35926 ) ) ;
#78829=CARTESIAN_POINT ( 'NONE',  ( -0.1742125984251974291, -0.1742125984251974014, -0.3937007874015748254 ) ) ;
#78901=FACE_OUTER_BOUND ( 'NONE', #68925, .T. ) ;
#79113=CARTESIAN_POINT ( 'NONE',  ( 0.2945512653497797673, 0.02373080790438491378, 5.526002588227517442 ) ) ;
#79188=VERTEX_POINT ( 'NONE', #21497 ) ;
#79229=CIRCLE ( 'NONE', #65764, 0.2952755905511810774 ) ;
#79265=DIRECTION ( 'NONE',  ( 1.000000000000000000, 8.805702923740138355E-17, -0.000000000000000000 ) ) ;
#79481=LINE ( 'NONE', #1622, #67382 ) ;
#79523=CARTESIAN_POINT ( 'NONE',  ( 0.2405540237485361554, 0.1712599301372657035, 5.748856329247439945 ) ) ;
#79566=DIRECTION ( 'NONE',  ( 0.000000000000000000, 0.000000000000000000, -1.000000000000000000 ) ) ;
#79596=CARTESIAN_POINT ( 'NONE',  ( 0.2943720246490709180, -0.02382778696830936682, 5.526312367533045666 ) ) ;
#79699=AXIS2_PLACEMENT_3D ( 'NONE', #10553, #55964, #23161 ) ;
#79727=DIRECTION ( 'NONE',  ( -1.000000000000000000, 0.000000000000000000, 0.000000000000000000 ) ) ;
#79739=VECTOR ( 'NONE', #79985, 39.37007874015748143 ) ;
#79943=CARTESIAN_POINT ( 'NONE',  ( 0.2597269936800725709, 0.1406511682536830121, 5.810287953473521227 ) ) ;
#79985=DIRECTION ( 'NONE',  ( 0.000000000000000000, -1.000000000000000000, 0.000000000000000000 ) ) ;
#80103=DIRECTION ( 'NONE',  ( 1.000000000000000000, 0.000000000000000000, -0.000000000000000000 ) ) ;
#80147=AXIS2_PLACEMENT_3D ( 'NONE', #30957, #71341, #76008 ) ;
#80338=B_SPLINE_CURVE_WITH_KNOTS ( 'NONE', 3,
 ( #2495, #27740, #79113, #40781, #47501, #47086, #2906, #55053, #72776, #53810, #28979, #28155, #66467, #60144, #74025, #60556, #48328, #41609, #8802, #28570, #34478, #34894, #41203, #79523, #21838, #73194, #60964, #79943, #15544, #15962, #9221, #54226, #16371, #35302, #54646, #10048, #35711, #61381, #3730, #63442 ),
 .UNSPECIFIED., .F., .F.,
 ( 4, 2, 2, 2, 2, 2, 2, 2, 2, 2, 2, 2, 2, 2, 2, 2, 2, 2, 2, 4 ),
 ( 0.01443715752414749184, 0.01533768712752721884, 0.01623821673090694584, 0.01713874633428667110, 0.01803927593766639637, 0.01893980554104612510, 0.01984033514442585036, 0.02029059994611567830, 0.02074086474780550277, 0.02119112954949533070, 0.02164139435118515517, 0.02254192395456481104, 0.02344245355794446345, 0.02434298316132411932, 0.02524351276470376826, 0.02614404236808342413, 0.02659430716977325554, 0.02704457197146308001, 0.02794510157484273241, 0.02884563117822238482 ),
 .UNSPECIFIED. ) ;
#80452=VECTOR ( 'NONE', #45688, 39.37007874015748143 ) ;
#80630=CARTESIAN_POINT ( 'NONE',  ( -0.1133856558944468518, -0.2726377952755905665, 0.1574803149606299191 ) ) ;
#80768=ORIENTED_EDGE ( 'NONE', *, *, #76404, .F. ) ;
#80770=CARTESIAN_POINT ( 'NONE',  ( -0.1970133122064499087, 0.2199809220305531388, 0.1374248322900813168 ) ) ;
#80803=CARTESIAN_POINT ( 'NONE',  ( -0.2726377952755906220, -0.1938976377952756625, 0.1574803149606299191 ) ) ;
#80974=DIRECTION ( 'NONE',  ( 0.000000000000000000, 0.000000000000000000, 1.000000000000000000 ) ) ;
#81093=EDGE_CURVE ( 'NONE', #23282, #52953, #8244, .T. ) ;
#81486=LINE ( 'NONE', #11605, #53148 ) ;
#81504=CARTESIAN_POINT ( 'NONE',  ( 0.000000000000000000, 0.000000000000000000, 0.1574803149606299191 ) ) ;
#81573=ORIENTED_EDGE ( 'NONE', *, *, #49711, .F. ) ;
#81662=EDGE_CURVE ( 'NONE', #2979, #51375, #19442, .T. ) ;
#81790=CARTESIAN_POINT ( 'NONE',  ( -0.2845468109762787079, -0.07963338598832103710, 5.543284456214096600 ) ) ;
#81826=CYLINDRICAL_SURFACE ( 'NONE', #30362, 0.1771653543307088186 ) ;
#81911=( NAMED_UNIT ( * ) PLANE_ANGLE_UNIT ( ) SI_UNIT ( $, .RADIAN. ) );
#82006=CARTESIAN_POINT ( 'NONE',  ( -0.1751536117528151582, 0.2379288306351265425, 0.1496817530000226215 ) ) ;
#82034=DIRECTION ( 'NONE',  ( -1.000000000000000000, -0.000000000000000000, -0.000000000000000000 ) ) ;
#82085=ORIENTED_EDGE ( 'NONE', *, *, #32628, .T. ) ;
#82158=CARTESIAN_POINT ( 'NONE',  ( 0.000000000000000000, 0.2726377952755905665, 0.07874015748031495954 ) ) ;
#82196=CARTESIAN_POINT ( 'NONE',  ( -0.2524556255358376688, -0.1533185143264484962, 5.612478741320920506 ) ) ;
#82209=CARTESIAN_POINT ( 'NONE',  ( 0.2952755905511810774, 3.616083068348483797E-17, 0.1574803149606299191 ) ) ;
#82313=EDGE_LOOP ( 'NONE', ( #3164, #23797, #82085, #63860 ) ) ;
#82328=EDGE_CURVE ( 'NONE', #70570, #16375, #35558, .T. ) ;
#82600=CARTESIAN_POINT ( 'NONE',  ( -0.2596871853482274894, -0.1407230452551245514, 5.593746434152945035 ) ) ;
#82750=ORIENTED_EDGE ( 'NONE', *, *, #34017, .T. ) ;
#82881=DIRECTION ( 'NONE',  ( 0.000000000000000000, -1.000000000000000000, 0.000000000000000000 ) ) ;
#82901=ORIENTED_EDGE ( 'NONE', *, *, #47017, .T. ) ;
#83053=CARTESIAN_POINT ( 'NONE',  ( 1.968503937007874072, 0.000000000000000000, 5.701968306260621233 ) ) ;
#83258=CARTESIAN_POINT ( 'NONE',  ( 0.2087913723976025926, 0.2087913723976026203, 0.1248231986745541033 ) ) ;
ENDSEC;
END-ISO-10303-21;
